ISO-10303-21;
HEADER;
FILE_DESCRIPTION (('STEP AP214'),
    '1' );
FILE_NAME ('Snap Open Cable Crossbars 6.step',
    '2026-10-08T22:59:04',
    ( '' ),
    ( '' ),
    'SwSTEP 2.0',
    'SolidWorks 2020',
    '' );
FILE_SCHEMA (( 'AUTOMOTIVE_DESIGN' ));
ENDSEC;

DATA;
#38=PLANE ( 'NONE',  #96833 ) ;
#121=DIRECTION ( 'NONE',  ( 1.000000000000000000, 0.000000000000000000, -0.000000000000000000 ) ) ;
#167=CARTESIAN_POINT ( 'NONE',  ( -18.39999999999999858, 11.47316190337362762, -176.8259460668079441 ) ) ;
#300=EDGE_CURVE ( 'NONE', #67768, #134738, #175812, .T. ) ;
#433=VERTEX_POINT ( 'NONE', #45265 ) ;
#436=CARTESIAN_POINT ( 'NONE',  ( -16.93211319090181988, 9.999986781168624717, -188.4225054992730293 ) ) ;
#928=CARTESIAN_POINT ( 'NONE',  ( -16.87304349924914604, 9.961745077968330975, -188.3890666750451999 ) ) ;
#990=EDGE_CURVE ( 'NONE', #220874, #195448, #229707, .T. ) ;
#1378=AXIS2_PLACEMENT_3D ( 'NONE', #246617, #163255, #23761 ) ;
#1384=LINE ( 'NONE', #163073, #68078 ) ;
#1511=ORIENTED_EDGE ( 'NONE', *, *, #236939, .T. ) ;
#1714=VERTEX_POINT ( 'NONE', #189958 ) ;
#1811=CARTESIAN_POINT ( 'NONE',  ( -16.87036670365549895, 9.989418819312803066, -180.0204398826979286 ) ) ;
#1875=EDGE_CURVE ( 'NONE', #220791, #75515, #120709, .T. ) ;
#2064=SURFACE_STYLE_FILL_AREA ( #162459 ) ;
#2103=CARTESIAN_POINT ( 'NONE',  ( -16.98495255085921229, 10.00556436600593280, -180.1346172062204687 ) ) ;
#2271=PLANE ( 'NONE',  #131101 ) ;
#2399=ORIENTED_EDGE ( 'NONE', *, *, #105194, .T. ) ;
#2425=AXIS2_PLACEMENT_3D ( 'NONE', #153513, #135160, #16531 ) ;
#2442=DIRECTION ( 'NONE',  ( 0.000000000000000000, 0.000000000000000000, 1.000000000000000000 ) ) ;
#2586=DIRECTION ( 'NONE',  ( 0.000000000000000000, 1.000000000000000000, 0.000000000000000000 ) ) ;
#2691=CARTESIAN_POINT ( 'NONE',  ( -16.92280123533699054, 9.950000000011137047, -180.3506323140850611 ) ) ;
#2699=DIRECTION ( 'NONE',  ( -1.000000000000000000, -0.000000000000000000, -0.000000000000000000 ) ) ;
#2708=VERTEX_POINT ( 'NONE', #45387 ) ;
#2805=VECTOR ( 'NONE', #224862, 1000.000000000000000 ) ;
#2936=DIRECTION ( 'NONE',  ( 1.000000000000000000, 0.000000000000000000, -0.000000000000000000 ) ) ;
#3064=CARTESIAN_POINT ( 'NONE',  ( -12.29659703204452192, 9.355888454513703323, -183.7886428967780148 ) ) ;
#3074=VECTOR ( 'NONE', #190597, 1000.000000000000000 ) ;
#3398=VECTOR ( 'NONE', #104015, 1000.000000000000000 ) ;
#3439=DIRECTION ( 'NONE',  ( -0.7071067811865456854, 0.7071067811865493491, 0.000000000000000000 ) ) ;
#3862=DIRECTION ( 'NONE',  ( -0.000000000000000000, 0.000000000000000000, -1.000000000000000000 ) ) ;
#3870=CARTESIAN_POINT ( 'NONE',  ( -16.88853107394619002, 9.950878483358135185, -188.3529363468922213 ) ) ;
#4231=CARTESIAN_POINT ( 'NONE',  ( -16.86379686415369861, 9.975217759264314310, -180.0666101109096928 ) ) ;
#4251=VERTEX_POINT ( 'NONE', #112805 ) ;
#4635=ORIENTED_EDGE ( 'NONE', *, *, #56654, .F. ) ;
#4669=FACE_OUTER_BOUND ( 'NONE', #170070, .T. ) ;
#4770=ADVANCED_FACE ( 'NONE', ( #257087 ), #174721, .F. ) ;
#4786=EDGE_CURVE ( 'NONE', #244261, #47603, #83599, .T. ) ;
#5061=CARTESIAN_POINT ( 'NONE',  ( 15.74999999999999645, 9.350000000011139178, -184.2499999999999716 ) ) ;
#5831=CARTESIAN_POINT ( 'NONE',  ( 13.88302573338719093, 9.457410944778567696, -182.5000839737900549 ) ) ;
#5849=EDGE_CURVE ( 'NONE', #220874, #255276, #171161, .T. ) ;
#6043=EDGE_CURVE ( 'NONE', #244261, #167528, #106925, .T. ) ;
#6088=DIRECTION ( 'NONE',  ( -1.000000000000000000, -1.646408749285562691E-14, 1.073024830501117725E-15 ) ) ;
#6157=VECTOR ( 'NONE', #130293, 1000.000000000000000 ) ;
#6247=FACE_OUTER_BOUND ( 'NONE', #245726, .T. ) ;
#6394=VERTEX_POINT ( 'NONE', #55962 ) ;
#6420=FACE_OUTER_BOUND ( 'NONE', #184848, .T. ) ;
#6884=EDGE_CURVE ( 'NONE', #185125, #224829, #184278, .T. ) ;
#6919=AXIS2_PLACEMENT_3D ( 'NONE', #250694, #147762, #72084 ) ;
#7123=CARTESIAN_POINT ( 'NONE',  ( 14.87567385445977131, 9.430764995433476017, -182.7305373947503995 ) ) ;
#7147=CARTESIAN_POINT ( 'NONE',  ( -16.97683809663752186, 9.850000000011137402, -187.5976359818036485 ) ) ;
#7435=DIRECTION ( 'NONE',  ( 1.000000000000000000, 1.186688945009010077E-16, 0.000000000000000000 ) ) ;
#7465=CARTESIAN_POINT ( 'NONE',  ( -17.11825945287481332, 10.05000000001113847, -188.2499999999999716 ) ) ;
#7544=ORIENTED_EDGE ( 'NONE', *, *, #143935, .F. ) ;
#7735=DIRECTION ( 'NONE',  ( 1.186688945009009831E-16, -1.000000000000000000, 0.000000000000000000 ) ) ;
#7753=CARTESIAN_POINT ( 'NONE',  ( -16.94275863009466576, 9.989496048673542461, -180.1083026179588558 ) ) ;
#7855=EDGE_CURVE ( 'NONE', #243110, #171479, #41406, .T. ) ;
#7890=ORIENTED_EDGE ( 'NONE', *, *, #124839, .T. ) ;
#7917=DIRECTION ( 'NONE',  ( 1.186688945009009831E-16, -1.000000000000000000, 0.000000000000000000 ) ) ;
#7968=CARTESIAN_POINT ( 'NONE',  ( -16.82055514392394713, 9.950000000011197443, -188.3232019254582212 ) ) ;
#8032=PLANE ( 'NONE',  #1378 ) ;
#8098=CARTESIAN_POINT ( 'NONE',  ( 23.24999999999999645, 11.75000000001113953, -176.7499999999999716 ) ) ;
#8313=( BOUNDED_SURFACE ( )  B_SPLINE_SURFACE ( 3, 2, ( 
 ( #207553, #194418, #219073 ),
 ( #96549, #58707, #213958 ),
 ( #256878, #135684, #15790 ),
 ( #139536, #77005, #176137 ) ),
 .UNSPECIFIED., .F., .F., .F. ) 
 B_SPLINE_SURFACE_WITH_KNOTS ( ( 4, 4 ),
 ( 3, 3 ),
 ( 0.0008258556059633754111, 0.0009616864997633037737 ),
 ( 0.000000000000000000, 1.000000000000000000 ),
 .UNSPECIFIED. ) 
 GEOMETRIC_REPRESENTATION_ITEM ( )  RATIONAL_B_SPLINE_SURFACE ( (
 ( 1.000000000000000000, 0.9152888060719425178, 1.000000000000000000),
 ( 1.000000000000000000, 0.9327727094137996389, 1.000000000000000000),
 ( 1.000000000000000000, 0.9369023509258144200, 1.000000000000000000),
 ( 1.000000000000000000, 0.9246339933864667904, 1.000000000000000000) ) ) 
 REPRESENTATION_ITEM ( '' )  SURFACE ( )  );
#8352=VERTEX_POINT ( 'NONE', #247183 ) ;
#8378=CIRCLE ( 'NONE', #154156, 0.5000000000000004441 ) ;
#8408=LINE ( 'NONE', #47506, #2805 ) ;
#8627=CARTESIAN_POINT ( 'NONE',  ( -17.78043020864321022, 10.85359211201684460, -190.6630491657201958 ) ) ;
#8766=EDGE_CURVE ( 'NONE', #68352, #179647, #20789, .T. ) ;
#8963=FACE_OUTER_BOUND ( 'NONE', #231454, .T. ) ;
#9028=CARTESIAN_POINT ( 'NONE',  ( -16.94333152886235894, 9.990342011461637028, -180.1079684689455576 ) ) ;
#9074=CARTESIAN_POINT ( 'NONE',  ( -16.85939681242906119, 9.905225185936460619, -188.0399219551914598 ) ) ;
#9131=CARTESIAN_POINT ( 'NONE',  ( -16.77431908686106254, 9.945805754529134290, -180.1641607823497395 ) ) ;
#9148=CARTESIAN_POINT ( 'NONE',  ( -18.34374000495059676, 11.47316190337362940, -191.7499999999999716 ) ) ;
#9167=CARTESIAN_POINT ( 'NONE',  ( 18.39999999999999503, 5.650000000011139001, -188.3499999999999659 ) ) ;
#9564=DIRECTION ( 'NONE',  ( -1.000000000000000000, 1.652117596168391700E-15, 0.000000000000000000 ) ) ;
#9610=ADVANCED_FACE ( 'NONE', ( #54162 ), #17593, .F. ) ;
#9761=CARTESIAN_POINT ( 'NONE',  ( 16.87683809663750267, 9.950000000011138823, -180.1499999999999773 ) ) ;
#10013=CARTESIAN_POINT ( 'NONE',  ( -16.87683809663752399, 21.23804903844422043, -180.1499999999999773 ) ) ;
#10084=ORIENTED_EDGE ( 'NONE', *, *, #71056, .F. ) ;
#10095=LINE ( 'NONE', #97288, #180120 ) ;
#10112=CARTESIAN_POINT ( 'NONE',  ( -12.60829076262180592, 9.389529397477895500, -185.3171079128936753 ) ) ;
#10291=ORIENTED_EDGE ( 'NONE', *, *, #128877, .F. ) ;
#10376=CARTESIAN_POINT ( 'NONE',  ( -16.77683809663752257, 9.945835743215303282, -188.3360509808957488 ) ) ;
#10419=CARTESIAN_POINT ( 'NONE',  ( -16.88783316861821859, 9.950000000011137047, -180.2522640419797426 ) ) ;
#10681=VERTEX_POINT ( 'NONE', #148423 ) ;
#10832=DIRECTION ( 'NONE',  ( -1.000000000000000000, 0.000000000000000000, 0.000000000000000000 ) ) ;
#10908=CARTESIAN_POINT ( 'NONE',  ( -16.81744102076749314, 9.950000000011142376, -180.1499999999999773 ) ) ;
#10911=CARTESIAN_POINT ( 'NONE',  ( -20.65000000000000568, 7.250000000011138646, -180.1499999999999773 ) ) ;
#10914=ADVANCED_FACE ( 'NONE', ( #136526 ), #98660, .F. ) ;
#11064=EDGE_LOOP ( 'NONE', ( #31607, #53064, #253982, #251293 ) ) ;
#11277=CARTESIAN_POINT ( 'NONE',  ( -16.94107738177414291, 10.01423928514777373, -188.4499999999999886 ) ) ;
#11330=LINE ( 'NONE', #32199, #214820 ) ;
#11405=CARTESIAN_POINT ( 'NONE',  ( -14.11361717019515538, 9.457426452500055092, -186.0000418683999612 ) ) ;
#11512=VECTOR ( 'NONE', #122509, 1000.000000000000000 ) ;
#11742=EDGE_CURVE ( 'NONE', #172479, #171479, #144581, .T. ) ;
#11818=EDGE_LOOP ( 'NONE', ( #183940, #128384, #54975, #15645, #61088, #243622, #248529, #45614, #171333, #147569, #140384, #222147, #248137, #189034, #194791, #225580, #33771, #12019 ) ) ;
#11871=EDGE_LOOP ( 'NONE', ( #61285, #212405, #117586, #30097, #106841, #7890 ) ) ;
#12019=ORIENTED_EDGE ( 'NONE', *, *, #66794, .T. ) ;
#12139=PLANE ( 'NONE',  #254002 ) ;
#12493=CARTESIAN_POINT ( 'NONE',  ( 12.26145404764308822, 9.351413679112544841, -184.4803435675489993 ) ) ;
#12552=VERTEX_POINT ( 'NONE', #167425 ) ;
#12703=CARTESIAN_POINT ( 'NONE',  ( -14.87770893841224940, 9.430637101707896264, -185.7682606180609355 ) ) ;
#12779=DIRECTION ( 'NONE',  ( -1.000000000000000000, 0.000000000000000000, 0.000000000000000000 ) ) ;
#12838=CARTESIAN_POINT ( 'NONE',  ( -16.27683809663750480, 9.350000000011133849, -176.7499999999999716 ) ) ;
#13006=ADVANCED_FACE ( 'NONE', ( #221900 ), #8032, .F. ) ;
#13029=ORIENTED_EDGE ( 'NONE', *, *, #6043, .T. ) ;
#13059=ORIENTED_EDGE ( 'NONE', *, *, #13784, .T. ) ;
#13080=CARTESIAN_POINT ( 'NONE',  ( -16.92989507731676113, 9.950000000011138823, -188.1174989306101395 ) ) ;
#13123=VERTEX_POINT ( 'NONE', #151399 ) ;
#13445=CARTESIAN_POINT ( 'NONE',  ( 16.87683809663749557, 9.950000000011131718, -188.3499999999999659 ) ) ;
#13602=ORIENTED_EDGE ( 'NONE', *, *, #254777, .F. ) ;
#13690=EDGE_CURVE ( 'NONE', #189000, #67768, #226412, .T. ) ;
#13753=EDGE_CURVE ( 'NONE', #171694, #6394, #51810, .T. ) ;
#13763=DIRECTION ( 'NONE',  ( -1.000000000000000000, 0.000000000000000000, 0.000000000000000000 ) ) ;
#13784=EDGE_CURVE ( 'NONE', #129693, #248393, #80645, .T. ) ;
#13877=VERTEX_POINT ( 'NONE', #95268 ) ;
#13926=AXIS2_PLACEMENT_3D ( 'NONE', #234408, #134027, #86224 ) ;
#13972=CARTESIAN_POINT ( 'NONE',  ( -15.39126916658603150, 9.389571634557567492, -185.3176407123691547 ) ) ;
#14011=EDGE_CURVE ( 'NONE', #151221, #34916, #255966, .T. ) ;
#14056=AXIS2_PLACEMENT_3D ( 'NONE', #77047, #222973, #204686 ) ;
#14221=DIRECTION ( 'NONE',  ( -1.000000000000000000, 0.000000000000000000, 0.000000000000000000 ) ) ;
#14690=VECTOR ( 'NONE', #236674, 1000.000000000000000 ) ;
#15423=CIRCLE ( 'NONE', #77931, 0.09999999999999939493 ) ;
#15506=AXIS2_PLACEMENT_3D ( 'NONE', #232409, #70774, #94147 ) ;
#15645=ORIENTED_EDGE ( 'NONE', *, *, #183746, .T. ) ;
#15790=CARTESIAN_POINT ( 'NONE',  ( -16.92973740335290245, 9.992503814478434165, -188.4060590352027873 ) ) ;
#15799=VECTOR ( 'NONE', #140525, 1000.000000000000000 ) ;
#16192=CARTESIAN_POINT ( 'NONE',  ( -16.93353400591625757, 10.00461239618409515, -188.4326844702054018 ) ) ;
#16224=ORIENTED_EDGE ( 'NONE', *, *, #25549, .T. ) ;
#16231=EDGE_LOOP ( 'NONE', ( #182843, #139904, #65165, #163755 ) ) ;
#16364=ADVANCED_FACE ( 'NONE', ( #87646 ), #109780, .T. ) ;
#16531=DIRECTION ( 'NONE',  ( 1.000000000000000000, 0.000000000000000000, 0.000000000000000000 ) ) ;
#17159=CARTESIAN_POINT ( 'NONE',  ( -16.94037747912386038, 10.01353938249748410, -180.0511309579754595 ) ) ;
#17207=EDGE_CURVE ( 'NONE', #241870, #12552, #100828, .T. ) ;
#17259=CARTESIAN_POINT ( 'NONE',  ( -16.87683809663752399, 9.850000000011139178, -187.5976359818036485 ) ) ;
#17429=CARTESIAN_POINT ( 'NONE',  ( -20.65000000000000568, 5.650000000011139001, -180.1499999999999773 ) ) ;
#17446=CARTESIAN_POINT ( 'NONE',  ( -16.93860193097148326, 9.993107767340401182, -188.4001383673068233 ) ) ;
#17503=CARTESIAN_POINT ( 'NONE',  ( -14.23072895065542731, 9.455987233623897481, -182.5115311668977824 ) ) ;
#17593=CYLINDRICAL_SURFACE ( 'NONE', #229010, 0.9000000000000014655 ) ;
#17671=FACE_OUTER_BOUND ( 'NONE', #246048, .T. ) ;
#17746=DIRECTION ( 'NONE',  ( -1.000000000000000000, 0.000000000000000000, 0.000000000000000000 ) ) ;
#17820=CIRCLE ( 'NONE', #230812, 1.500000000000001332 ) ;
#17832=CIRCLE ( 'NONE', #142903, 0.9000000000000014655 ) ;
#17966=DIRECTION ( 'NONE',  ( 0.8049926720990051576, 0.5932847527679298016, -0.000000000000000000 ) ) ;
#18137=CARTESIAN_POINT ( 'NONE',  ( -21.64999999999999858, 9.350000000011133849, -188.3499999999999659 ) ) ;
#18410=ORIENTED_EDGE ( 'NONE', *, *, #237291, .F. ) ;
#18712=ORIENTED_EDGE ( 'NONE', *, *, #37330, .T. ) ;
#18758=LINE ( 'NONE', #120468, #105170 ) ;
#18791=CARTESIAN_POINT ( 'NONE',  ( 20.99999999999999645, 9.750000000011137757, -176.7499999999999716 ) ) ;
#19116=CARTESIAN_POINT ( 'NONE',  ( -17.04761207306821191, 10.02645087340893326, -180.1499999999999488 ) ) ;
#19337=CARTESIAN_POINT ( 'NONE',  ( -16.94445028196807002, 9.992063609708893068, -188.3926698215815350 ) ) ;
#19585=DIRECTION ( 'NONE',  ( -0.7071067811865463515, 0.7071067811865487940, -0.000000000000000000 ) ) ;
#19796=CARTESIAN_POINT ( 'NONE',  ( -18.40000000000000213, 11.75000000001113953, -188.3499999999999659 ) ) ;
#19798=ORIENTED_EDGE ( 'NONE', *, *, #13784, .F. ) ;
#19833=CARTESIAN_POINT ( 'NONE',  ( -16.85697194749122829, 9.908543714134735225, -188.0649957323861656 ) ) ;
#20103=LINE ( 'NONE', #99594, #135156 ) ;
#20152=DIRECTION ( 'NONE',  ( -1.073024830501117725E-15, 0.000000000000000000, 1.000000000000000000 ) ) ;
#20167=DIRECTION ( 'NONE',  ( -1.073024830501117725E-15, -0.000000000000000000, -1.000000000000000000 ) ) ;
#20591=VECTOR ( 'NONE', #22799, 1000.000000000000000 ) ;
#20721=EDGE_CURVE ( 'NONE', #100115, #192577, #69499, .T. ) ;
#20724=DIRECTION ( 'NONE',  ( 1.186688945009010077E-16, -1.000000000000000000, -0.000000000000000000 ) ) ;
#20789=B_SPLINE_CURVE_WITH_KNOTS ( 'NONE', 3,
 ( #59898, #119936, #199457, #258075, #97732, #254251, #74392, #198145, #195610, #117333 ),
 .UNSPECIFIED., .F., .F.,
 ( 4, 3, 3, 4 ),
 ( -2.000561356219677529E-06, 0.000000000000000000, 1.787822682429502760E-05, 4.206475347090109142E-05 ),
 .UNSPECIFIED. ) ;
#20898=CARTESIAN_POINT ( 'NONE',  ( -16.88005004766534967, 9.950100503332199864, -188.3503361119487352 ) ) ;
#20925=EDGE_CURVE ( 'NONE', #243110, #1714, #137809, .T. ) ;
#20948=EDGE_CURVE ( 'NONE', #171479, #108576, #149329, .T. ) ;
#21062=B_SPLINE_CURVE_WITH_KNOTS ( 'NONE', 3,
 ( #109862, #47311, #87727, #26505, #30360, #29105, #168626, #146411, #49898, #27810, #69490, #90297, #169906, #250660 ),
 .UNSPECIFIED., .F., .F.,
 ( 4, 2, 2, 2, 2, 2, 4 ),
 ( 0.000000000000000000, 2.389617747639151307E-05, 4.779235495278302614E-05, 9.558470990564444010E-05, 0.0001911694198113644762, 0.0003823388396228028950, 0.0007646776792455974416 ),
 .UNSPECIFIED. ) ;
#21256=ORIENTED_EDGE ( 'NONE', *, *, #82133, .F. ) ;
#21320=LINE ( 'NONE', #202496, #94611 ) ;
#21340=ORIENTED_EDGE ( 'NONE', *, *, #213599, .T. ) ;
#21432=ORIENTED_EDGE ( 'NONE', *, *, #37330, .F. ) ;
#21665=DIRECTION ( 'NONE',  ( -0.8049926720990042694, -0.5932847527679310229, 0.000000000000000000 ) ) ;
#21820=ORIENTED_EDGE ( 'NONE', *, *, #8766, .F. ) ;
#21822=FACE_OUTER_BOUND ( 'NONE', #23756, .T. ) ;
#21824=CARTESIAN_POINT ( 'NONE',  ( -16.88460203013676875, 9.954759003246872240, -188.3658918095381978 ) ) ;
#21883=CARTESIAN_POINT ( 'NONE',  ( 18.54999999999999716, 8.750000000011182166, -180.1499999999999773 ) ) ;
#21916=CARTESIAN_POINT ( 'NONE',  ( -16.94107738177415712, 10.01423928514777728, -180.0499999999999545 ) ) ;
#22041=VERTEX_POINT ( 'NONE', #55200 ) ;
#22172=CARTESIAN_POINT ( 'NONE',  ( -16.89268316805465986, 9.951721813253337601, -188.3557524785454973 ) ) ;
#22307=VERTEX_POINT ( 'NONE', #45825 ) ;
#22327=FACE_OUTER_BOUND ( 'NONE', #131692, .T. ) ;
#22544=CARTESIAN_POINT ( 'NONE',  ( -16.86337532320262156, 9.979967204235514089, -180.0510755310171476 ) ) ;
#22670=DIRECTION ( 'NONE',  ( -0.000000000000000000, -0.000000000000000000, -1.000000000000000000 ) ) ;
#22676=CARTESIAN_POINT ( 'NONE',  ( -12.47155713865591942, 9.375669526436931633, -183.3677900093859705 ) ) ;
#22799=DIRECTION ( 'NONE',  ( -1.000000000000000000, 0.000000000000000000, 0.000000000000000000 ) ) ;
#22878=CARTESIAN_POINT ( 'NONE',  ( 14.56326696814970845, 9.446648990640015953, -182.5891632959231288 ) ) ;
#23015=VECTOR ( 'NONE', #142469, 1000.000000000000000 ) ;
#23120=CARTESIAN_POINT ( 'NONE',  ( -18.44085059012132177, 11.51401249349496325, -191.7403053191215179 ) ) ;
#23128=STYLED_ITEM ( 'NONE', ( #158620 ), #73277 ) ;
#23362=VECTOR ( 'NONE', #246564, 1000.000000000000000 ) ;
#23588=CARTESIAN_POINT ( 'NONE',  ( -16.77683809663752257, 9.945835743215301505, -180.1639490191041943 ) ) ;
#23700=CARTESIAN_POINT ( 'NONE',  ( -16.77308656112215601, 9.950000000011133494, -188.3498068082976431 ) ) ;
#23753=CIRCLE ( 'NONE', #169499, 0.09999999999999939493 ) ;
#23756=EDGE_LOOP ( 'NONE', ( #77803, #50328, #103182, #165089, #111690 ) ) ;
#23761=DIRECTION ( 'NONE',  ( 0.000000000000000000, -0.000000000000000000, -1.000000000000000000 ) ) ;
#24154=CARTESIAN_POINT ( 'NONE',  ( 12.84233041328156766, 9.410538608540022665, -182.9326879971409028 ) ) ;
#24237=ORIENTED_EDGE ( 'NONE', *, *, #248993, .F. ) ;
#24353=CARTESIAN_POINT ( 'NONE',  ( -17.29158576265543346, 10.36474766602906961, -189.5827582447921600 ) ) ;
#24522=DIRECTION ( 'NONE',  ( 0.000000000000000000, 0.000000000000000000, 1.000000000000000000 ) ) ;
#24526=VECTOR ( 'NONE', #142499, 1000.000000000000000 ) ;
#24623=DIRECTION ( 'NONE',  ( 0.000000000000000000, 1.000000000000000000, -0.000000000000000000 ) ) ;
#24860=CARTESIAN_POINT ( 'NONE',  ( -16.80438519320023616, 9.949779096479501206, -180.1507382809212743 ) ) ;
#25075=TOROIDAL_SURFACE ( 'NONE', #129103, 14.20833333333334103, 0.1000000000000000056 ) ;
#25228=CARTESIAN_POINT ( 'NONE',  ( -16.97683809663752186, 9.850000000011137402, -180.9023640181964652 ) ) ;
#25434=CARTESIAN_POINT ( 'NONE',  ( 12.25000000000000178, 9.350000000011142731, -184.0215193718251214 ) ) ;
#25455=DIRECTION ( 'NONE',  ( 0.000000000000000000, 0.000000000000000000, -1.000000000000000000 ) ) ;
#25549=EDGE_CURVE ( 'NONE', #94057, #13123, #17820, .T. ) ;
#25623=VERTEX_POINT ( 'NONE', #196310 ) ;
#25738=EDGE_LOOP ( 'NONE', ( #255660, #203485, #109182, #243584 ) ) ;
#25816=VECTOR ( 'NONE', #2699, 1000.000000000000000 ) ;
#25821=VECTOR ( 'NONE', #108043, 1000.000000000000000 ) ;
#25837=CARTESIAN_POINT ( 'NONE',  ( -16.94107738177415357, 10.01423928514777728, -180.0499999999999545 ) ) ;
#25897=LINE ( 'NONE', #105376, #150230 ) ;
#25932=CARTESIAN_POINT ( 'NONE',  ( 22.88900146558018989, 8.703904791123973084, -180.1499999999999773 ) ) ;
#26085=ORIENTED_EDGE ( 'NONE', *, *, #34149, .T. ) ;
#26135=CARTESIAN_POINT ( 'NONE',  ( -16.89935556175703368, 9.950000000011137047, -180.6396763628857514 ) ) ;
#26249=CARTESIAN_POINT ( 'NONE',  ( -16.77180007708461318, 9.950000000011137047, -188.3643858810451377 ) ) ;
#26474=DIRECTION ( 'NONE',  ( -0.7071067811865463515, -0.7071067811865487940, 7.587431340288849180E-16 ) ) ;
#26505=CARTESIAN_POINT ( 'NONE',  ( -16.80100426158789872, 9.943150520407291637, -180.1829457528340015 ) ) ;
#26509=DIRECTION ( 'NONE',  ( -1.000000000000000000, 0.000000000000000000, 0.000000000000000000 ) ) ;
#27058=LINE ( 'NONE', #105229, #211479 ) ;
#27194=ORIENTED_EDGE ( 'NONE', *, *, #71887, .T. ) ;
#27208=CARTESIAN_POINT ( 'NONE',  ( -16.98495255085916966, 10.00556436600592214, -188.3653827937794745 ) ) ;
#27587=EDGE_CURVE ( 'NONE', #171571, #43357, #71216, .T. ) ;
#27588=CARTESIAN_POINT ( 'NONE',  ( 18.39999999999997371, 11.75000000001113953, -176.7499999999999716 ) ) ;
#27810=CARTESIAN_POINT ( 'NONE',  ( -16.85312841634287651, 9.913606177331363511, -180.3971731332925970 ) ) ;
#27865=DIRECTION ( 'NONE',  ( -1.646408749285562691E-14, 1.000000000000000000, 0.000000000000000000 ) ) ;
#27930=CARTESIAN_POINT ( 'NONE',  ( 20.99999999999999645, 9.750000000011137757, -180.1499999999999773 ) ) ;
#28185=PLANE ( 'NONE',  #240527 ) ;
#28259=EDGE_CURVE ( 'NONE', #222610, #158360, #28947, .T. ) ;
#28590=DIRECTION ( 'NONE',  ( 1.186688945009009831E-16, -1.000000000000000000, 0.000000000000000000 ) ) ;
#28725=MECHANICAL_DESIGN_GEOMETRIC_PRESENTATION_REPRESENTATION('',(#137011),#132753);
#28731=CARTESIAN_POINT ( 'NONE',  ( -16.78055652883087134, 9.946776916136505164, -180.1607918375923987 ) ) ;
#28947=LINE ( 'NONE', #48451, #48149 ) ;
#28983=CARTESIAN_POINT ( 'NONE',  ( -18.40000000000000213, 8.822561741677553471, -191.7499999999999716 ) ) ;
#29105=CARTESIAN_POINT ( 'NONE',  ( -16.81453046979148880, 9.939102281452070642, -180.2117265236030050 ) ) ;
#29173=ORIENTED_EDGE ( 'NONE', *, *, #169248, .F. ) ;
#29266=EDGE_CURVE ( 'NONE', #33770, #108576, #104587, .T. ) ;
#29304=PLANE ( 'NONE',  #140154 ) ;
#29386=EDGE_CURVE ( 'NONE', #255276, #43357, #87601, .T. ) ;
#29397=ORIENTED_EDGE ( 'NONE', *, *, #135873, .T. ) ;
#29420=CARTESIAN_POINT ( 'NONE',  ( -16.87036670365548474, 9.989418819312801290, -188.4795601173020145 ) ) ;
#29506=CARTESIAN_POINT ( 'NONE',  ( 12.93279065517211635, 9.417690691074255938, -185.6416006967645842 ) ) ;
#29649=EDGE_CURVE ( 'NONE', #8352, #151091, #44355, .T. ) ;
#29704=CARTESIAN_POINT ( 'NONE',  ( -14.22969084473441193, 9.456007326080463571, -185.9886334941467396 ) ) ;
#30097=ORIENTED_EDGE ( 'NONE', *, *, #169248, .T. ) ;
#30133=VECTOR ( 'NONE', #43235, 1000.000000000000000 ) ;
#30217=CARTESIAN_POINT ( 'NONE',  ( 18.39999999999999503, 5.650000000011139001, -180.1499999999999773 ) ) ;
#30231=CARTESIAN_POINT ( 'NONE',  ( -16.87683809663752399, 9.950000000011142376, -180.1499999999999773 ) ) ;
#30360=CARTESIAN_POINT ( 'NONE',  ( -16.80468759584937644, 9.942153675145295466, -180.1900188662016546 ) ) ;
#30476=ORIENTED_EDGE ( 'NONE', *, *, #49144, .F. ) ;
#30570=VERTEX_POINT ( 'NONE', #58777 ) ;
#30696=VECTOR ( 'NONE', #17746, 1000.000000000000000 ) ;
#30779=CARTESIAN_POINT ( 'NONE',  ( 12.25000000000000000, 9.350000000011140955, -184.2499999999999716 ) ) ;
#31330=VERTEX_POINT ( 'NONE', #139485 ) ;
#31426=DIRECTION ( 'NONE',  ( -1.020425574104004196E-15, 0.000000000000000000, -1.000000000000000000 ) ) ;
#31479=CARTESIAN_POINT ( 'NONE',  ( 20.04999999999999716, 8.750000000011173285, -180.1499999999999773 ) ) ;
#31607=ORIENTED_EDGE ( 'NONE', *, *, #34149, .F. ) ;
#31753=EDGE_CURVE ( 'NONE', #231369, #146114, #244377, .T. ) ;
#31981=ORIENTED_EDGE ( 'NONE', *, *, #256129, .F. ) ;
#32062=CARTESIAN_POINT ( 'NONE',  ( 14.45963434102924694, 9.451541661396671401, -185.9538754988305698 ) ) ;
#32138=CARTESIAN_POINT ( 'NONE',  ( 20.04999999999999716, 8.750000000011173285, -188.3499999999999659 ) ) ;
#32199=CARTESIAN_POINT ( 'NONE',  ( 18.39999999999999503, 5.650000000011139001, -180.1499999999999773 ) ) ;
#32475=EDGE_CURVE ( 'NONE', #433, #68352, #177280, .T. ) ;
#32482=ORIENTED_EDGE ( 'NONE', *, *, #213599, .F. ) ;
#32550=DIRECTION ( 'NONE',  ( 1.073024830501117725E-15, 0.000000000000000000, 1.000000000000000000 ) ) ;
#32579=ORIENTED_EDGE ( 'NONE', *, *, #98097, .F. ) ;
#32580=CARTESIAN_POINT ( 'NONE',  ( -16.87401514999234919, 9.950000000011137047, -180.2199820074678769 ) ) ;
#33007=COLOUR_RGB ( '', 0.09019608, 0.27058824, 0.51372549) ;
#33184=ADVANCED_FACE ( 'NONE', ( #72549 ), #230311, .F. ) ;
#33345=EDGE_CURVE ( 'NONE', #42862, #25623, #8408, .T. ) ;
#33535=DIRECTION ( 'NONE',  ( 1.000000000000000000, 0.000000000000000000, 0.000000000000000000 ) ) ;
#33637=VECTOR ( 'NONE', #124848, 1000.000000000000000 ) ;
#33770=VERTEX_POINT ( 'NONE', #170760 ) ;
#33771=ORIENTED_EDGE ( 'NONE', *, *, #31753, .F. ) ;
#33910=DIRECTION ( 'NONE',  ( 1.000000000000000000, 0.000000000000000000, -0.000000000000000000 ) ) ;
#33922=FACE_OUTER_BOUND ( 'NONE', #81662, .T. ) ;
#33946=ADVANCED_FACE ( 'NONE', ( #212416 ), #157600, .T. ) ;
#34149=EDGE_CURVE ( 'NONE', #6394, #94057, #27058, .T. ) ;
#34671=EDGE_CURVE ( 'NONE', #108576, #154572, #190384, .T. ) ;
#34711=DIRECTION ( 'NONE',  ( 0.000000000000000000, 0.000000000000000000, -1.000000000000000000 ) ) ;
#34814=AXIS2_PLACEMENT_3D ( 'NONE', #92168, #231701, #33535 ) ;
#34916=VERTEX_POINT ( 'NONE', #91873 ) ;
#35217=DIRECTION ( 'NONE',  ( 0.000000000000000000, 0.000000000000000000, -1.000000000000000000 ) ) ;
#35225=CARTESIAN_POINT ( 'NONE',  ( -16.94226253665225812, 9.950000000011138823, -188.0532654043842342 ) ) ;
#35367=B_SPLINE_CURVE_WITH_KNOTS ( 'NONE', 3,
 ( #135556, #113440, #230846, #92578, #212559, #13080, #35225, #136848, #156460, #192989 ),
 .UNSPECIFIED., .F., .F.,
 ( 4, 2, 2, 2, 4 ),
 ( 5.247129907028296623E-16, 9.930191194499898442E-05, 0.0001986038238894732421, 0.0003972076477784217846, 0.0007944152955563189237 ),
 .UNSPECIFIED. ) ;
#35472=FACE_OUTER_BOUND ( 'NONE', #241576, .T. ) ;
#35596=CARTESIAN_POINT ( 'NONE',  ( -16.87036670365548474, 9.989418819312801290, -188.4795601173020145 ) ) ;
#35742=DIRECTION ( 'NONE',  ( 0.000000000000000000, 0.000000000000000000, 1.000000000000000000 ) ) ;
#35757=CARTESIAN_POINT ( 'NONE',  ( -16.93344882324368683, 9.996588767299030565, -188.4130256948049009 ) ) ;
#36359=CARTESIAN_POINT ( 'NONE',  ( -16.92570016628984320, 9.958788957751020021, -180.1206506700389411 ) ) ;
#37075=DIRECTION ( 'NONE',  ( -1.000000000000000000, 0.000000000000000000, 0.000000000000000000 ) ) ;
#37159=CARTESIAN_POINT ( 'NONE',  ( 18.39999999999999503, 11.47316190337363828, -191.7499999999999716 ) ) ;
#37330=EDGE_CURVE ( 'NONE', #77200, #104626, #8378, .T. ) ;
#37369=ORIENTED_EDGE ( 'NONE', *, *, #159690, .T. ) ;
#37400=DIRECTION ( 'NONE',  ( 1.000000000000000000, 1.186688945009010077E-16, 0.000000000000000000 ) ) ;
#37417=CARTESIAN_POINT ( 'NONE',  ( -17.11825945287482753, 10.05000000001113847, -180.1499999999999773 ) ) ;
#37514=ORIENTED_EDGE ( 'NONE', *, *, #6884, .T. ) ;
#37640=ORIENTED_EDGE ( 'NONE', *, *, #205750, .T. ) ;
#37730=VECTOR ( 'NONE', #171284, 1000.000000000000000 ) ;
#37862=AXIS2_PLACEMENT_3D ( 'NONE', #143523, #159263, #198366 ) ;
#37918=CARTESIAN_POINT ( 'NONE',  ( -18.40000000000000213, 11.47867410001105526, -191.7253067836593630 ) ) ;
#38054=AXIS2_PLACEMENT_3D ( 'NONE', #119485, #21665, #89315 ) ;
#38420=DIRECTION ( 'NONE',  ( 1.000000000000000000, 0.000000000000000000, 0.000000000000000000 ) ) ;
#39058=ORIENTED_EDGE ( 'NONE', *, *, #105567, .T. ) ;
#39080=APPLICATION_CONTEXT ( 'automotive_design' ) ;
#39112=CARTESIAN_POINT ( 'NONE',  ( 15.66039659514495419, 9.360749169926259938, -184.8145701406072021 ) ) ;
#39145=ORIENTED_EDGE ( 'NONE', *, *, #211512, .T. ) ;
#39544=CARTESIAN_POINT ( 'NONE',  ( -16.92507428761702926, 9.950000000011137047, -180.2133974596215467 ) ) ;
#39602=EDGE_CURVE ( 'NONE', #25623, #8352, #66377, .T. ) ;
#39620=CARTESIAN_POINT ( 'NONE',  ( -16.93826681692523195, 10.01142872029886632, -188.4454584673594013 ) ) ;
#39675=CARTESIAN_POINT ( 'NONE',  ( -15.06774609480955718, 9.417651958852163219, -182.8587873924404335 ) ) ;
#39815=DIRECTION ( 'NONE',  ( -1.000000000000000000, 0.000000000000000000, 0.000000000000000000 ) ) ;
#40018=DIRECTION ( 'NONE',  ( 0.000000000000000000, -1.000000000000000000, 0.000000000000000000 ) ) ;
#40068=LINE ( 'NONE', #158730, #221448 ) ;
#40211=CARTESIAN_POINT ( 'NONE',  ( -16.92973740335371247, 9.992503814478531865, -180.0939409647977527 ) ) ;
#40530=EDGE_CURVE ( 'NONE', #154572, #1714, #124891, .T. ) ;
#40590=CARTESIAN_POINT ( 'NONE',  ( -16.93230518875208546, 10.00075036143099894, -180.0757783481014940 ) ) ;
#40615=EDGE_CURVE ( 'NONE', #181967, #31330, #237353, .T. ) ;
#40622=EDGE_CURVE ( 'NONE', #116420, #13877, #62568, .T. ) ;
#40704=CARTESIAN_POINT ( 'NONE',  ( -16.83233564386398839, 9.930221796595855466, -188.2245206634760564 ) ) ;
#40960=CARTESIAN_POINT ( 'NONE',  ( -13.22483237240079745, 9.436674251854007878, -182.6768619309992232 ) ) ;
#41402=CARTESIAN_POINT ( 'NONE',  ( -16.89268316805465986, 9.951721813253337601, -188.3557524785454973 ) ) ;
#41406=( BOUNDED_CURVE ( )  B_SPLINE_CURVE ( 3, ( #145821, #27208, #188809, #46721 ),
 .UNSPECIFIED., .F., .T. ) 
 B_SPLINE_CURVE_WITH_KNOTS ( ( 4, 4 ),
 ( 3.752122642744613046, 4.712388980384671910 ),
 .UNSPECIFIED. ) 
 CURVE ( )  GEOMETRIC_REPRESENTATION_ITEM ( )  RATIONAL_B_SPLINE_CURVE ( ( 1.000000000000000000, 0.9246222802177266331, 0.9246222802177266331, 1.000000000000000000 ) ) 
 REPRESENTATION_ITEM ( '' )  );
#41487=CARTESIAN_POINT ( 'NONE',  ( -16.93301857435213620, 9.976309354746611291, -188.3857755711613891 ) ) ;
#41613=CARTESIAN_POINT ( 'NONE',  ( -20.65000000000000568, 5.650000000011139001, -176.7499999999999716 ) ) ;
#41726=PLANE ( 'NONE',  #91032 ) ;
#41806=CARTESIAN_POINT ( 'NONE',  ( -18.35663730107557257, 11.47390742652235573, -176.7499999999999716 ) ) ;
#41873=CARTESIAN_POINT ( 'NONE',  ( -18.40000000000000213, 5.650000000011139001, -180.1499999999999773 ) ) ;
#42223=CARTESIAN_POINT ( 'NONE',  ( -12.93407622233968368, 9.417789466963364831, -182.8573845439768775 ) ) ;
#42233=EDGE_CURVE ( 'NONE', #241870, #220791, #65929, .T. ) ;
#42502=CARTESIAN_POINT ( 'NONE',  ( -16.77683809663752257, 23.65833333334447985, -184.2499999999999716 ) ) ;
#42842=ADVANCED_FACE ( 'NONE', ( #181118 ), #239797, .F. ) ;
#42862=VERTEX_POINT ( 'NONE', #242348 ) ;
#42997=DIRECTION ( 'NONE',  ( 1.000000000000000000, 0.000000000000000000, -0.000000000000000000 ) ) ;
#43014=CARTESIAN_POINT ( 'NONE',  ( -16.77683809663752257, 9.945835743215303282, -188.3360509808957488 ) ) ;
#43046=VERTEX_POINT ( 'NONE', #235612 ) ;
#43149=SURFACE_STYLE_USAGE ( .BOTH. , #182668 ) ;
#43235=DIRECTION ( 'NONE',  ( -0.7071067811865456854, 0.7071067811865493491, 0.000000000000000000 ) ) ;
#43357=VERTEX_POINT ( 'NONE', #151957 ) ;
#43836=ORIENTED_EDGE ( 'NONE', *, *, #239552, .F. ) ;
#44355=LINE ( 'NONE', #243819, #230710 ) ;
#44436=PRESENTATION_STYLE_ASSIGNMENT (( #43149 ) ) ;
#44494=AXIS2_PLACEMENT_3D ( 'NONE', #159349, #255812, #194635 ) ;
#44854=( BOUNDED_CURVE ( )  B_SPLINE_CURVE ( 3, ( #138569, #39544, #110708, #103313 ),
 .UNSPECIFIED., .F., .F. ) 
 B_SPLINE_CURVE_WITH_KNOTS ( ( 4, 4 ),
 ( 0.5235987755983901870, 1.570796326794896558 ),
 .UNSPECIFIED. ) 
 CURVE ( )  GEOMETRIC_REPRESENTATION_ITEM ( )  RATIONAL_B_SPLINE_CURVE ( ( 1.000000000000000000, 0.9106836025229743115, 0.9106836025229743115, 1.000000000000000000 ) ) 
 REPRESENTATION_ITEM ( '' )  );
#45044=CARTESIAN_POINT ( 'NONE',  ( -17.01473183483381391, 9.950000000011138823, -188.2499999999999716 ) ) ;
#45225=CARTESIAN_POINT ( 'NONE',  ( -17.22767730081687887, 10.34924421247923654, -189.6424286905727286 ) ) ;
#45265=CARTESIAN_POINT ( 'NONE',  ( -16.77683809663752257, 9.945835743215301505, -180.1639490191041943 ) ) ;
#45355=ADVANCED_FACE ( 'NONE', ( #6247 ), #188831, .T. ) ;
#45361=ORIENTED_EDGE ( 'NONE', *, *, #97611, .F. ) ;
#45387=CARTESIAN_POINT ( 'NONE',  ( -21.65000000000000213, 7.250000000011139534, -188.3499999999999659 ) ) ;
#45472=ORIENTED_EDGE ( 'NONE', *, *, #237291, .T. ) ;
#45503=CARTESIAN_POINT ( 'NONE',  ( 12.48201962039796342, 9.376659938544690931, -185.1281925482172426 ) ) ;
#45614=ORIENTED_EDGE ( 'NONE', *, *, #40530, .T. ) ;
#45641=CARTESIAN_POINT ( 'NONE',  ( -16.87683809663752754, 9.864913447291344895, -187.7242815513039602 ) ) ;
#45825=CARTESIAN_POINT ( 'NONE',  ( -16.87331047859651179, 9.950000000011142376, -180.1499999999999773 ) ) ;
#46254=CARTESIAN_POINT ( 'NONE',  ( 14.22821877134046886, 9.456028260519072859, -182.5111980350657177 ) ) ;
#46571=DIRECTION ( 'NONE',  ( -0.000000000000000000, -0.000000000000000000, -1.000000000000000000 ) ) ;
#46721=CARTESIAN_POINT ( 'NONE',  ( -17.11825945287481332, 10.05000000001113847, -188.3499999999999659 ) ) ;
#46779=CARTESIAN_POINT ( 'NONE',  ( -18.34374000495059676, 11.47316190337362940, -191.7499999999999716 ) ) ;
#46857=CARTESIAN_POINT ( 'NONE',  ( -17.11825945287482753, 10.05000000001113847, -180.1499999999999773 ) ) ;
#46935=CARTESIAN_POINT ( 'NONE',  ( -16.78569801330232281, 9.947933733124651567, -180.1569129053474683 ) ) ;
#46992=VERTEX_POINT ( 'NONE', #201397 ) ;
#47311=CARTESIAN_POINT ( 'NONE',  ( -16.78493832629887095, 9.945835743215301505, -180.1639490191041943 ) ) ;
#47400=ORIENTED_EDGE ( 'NONE', *, *, #40622, .F. ) ;
#47456=EDGE_LOOP ( 'NONE', ( #84174, #155108, #65658, #227405, #235221 ) ) ;
#47506=CARTESIAN_POINT ( 'NONE',  ( 23.24999999999999645, 5.650000000011139001, -180.1499999999999773 ) ) ;
#47603=VERTEX_POINT ( 'NONE', #93981 ) ;
#47642=EDGE_CURVE ( 'NONE', #34916, #151221, #251519, .T. ) ;
#47675=EDGE_LOOP ( 'NONE', ( #53322, #84991, #37640, #21340 ) ) ;
#47697=FACE_OUTER_BOUND ( 'NONE', #185435, .T. ) ;
#48149=VECTOR ( 'NONE', #168462, 1000.000000000000000 ) ;
#48196=CARTESIAN_POINT ( 'NONE',  ( -16.87683809663752399, 9.850000000011144508, -187.5976359818036769 ) ) ;
#48209=VECTOR ( 'NONE', #162574, 1000.000000000000000 ) ;
#48223=ADVANCED_FACE ( 'NONE', ( #110042 ), #62409, .T. ) ;
#48248=CARTESIAN_POINT ( 'NONE',  ( -16.77180007708460252, 9.950000000011137047, -180.1356141189547770 ) ) ;
#48328=ORIENTED_EDGE ( 'NONE', *, *, #63203, .F. ) ;
#48451=CARTESIAN_POINT ( 'NONE',  ( -18.40000000000000213, 8.822561741677553471, -176.7499999999999716 ) ) ;
#48497=DIRECTION ( 'NONE',  ( 1.000000000000000000, 0.000000000000000000, 0.000000000000000000 ) ) ;
#48507=CARTESIAN_POINT ( 'NONE',  ( -16.86578989773641979, 9.984809801269951990, -180.0353351133777551 ) ) ;
#49110=DIRECTION ( 'NONE',  ( 1.186688945009009831E-16, -1.000000000000000000, 0.000000000000000000 ) ) ;
#49144=EDGE_CURVE ( 'NONE', #211794, #116420, #15423, .T. ) ;
#49488=CARTESIAN_POINT ( 'NONE',  ( -16.81453563122428108, 9.939100205448106351, -188.2882586606452833 ) ) ;
#49538=CARTESIAN_POINT ( 'NONE',  ( -16.85722902420155833, 9.950000000011137047, -180.2655474737702548 ) ) ;
#49556=ORIENTED_EDGE ( 'NONE', *, *, #100642, .T. ) ;
#49723=DIRECTION ( 'NONE',  ( -1.000000000000000000, 0.000000000000000000, 0.000000000000000000 ) ) ;
#49775=DIRECTION ( 'NONE',  ( 1.000000000000000000, -0.000000000000000000, -0.000000000000000000 ) ) ;
#49898=CARTESIAN_POINT ( 'NONE',  ( -16.83794237512073977, 9.926359221118634224, -180.3035421586989457 ) ) ;
#50294=CARTESIAN_POINT ( 'NONE',  ( 12.42718393586867087, 9.370655051134642477, -185.0258232559808960 ) ) ;
#50328=ORIENTED_EDGE ( 'NONE', *, *, #187437, .F. ) ;
#50349=UNCERTAINTY_MEASURE_WITH_UNIT (LENGTH_MEASURE( 1.000000000000000082E-05 ), #161166, 'distance_accuracy_value', 'NONE');
#50434=ORIENTED_EDGE ( 'NONE', *, *, #252724, .F. ) ;
#50489=CARTESIAN_POINT ( 'NONE',  ( -12.42749937872396870, 9.370689921613765350, -185.0264651266610088 ) ) ;
#50723=VECTOR ( 'NONE', #117511, 1000.000000000000000 ) ;
#50865=CARTESIAN_POINT ( 'NONE',  ( 16.27683809663749770, 9.350000000011137402, -176.7499999999999716 ) ) ;
#50912=CARTESIAN_POINT ( 'NONE',  ( -21.65000000000000213, 10.05000000001113847, -188.3499999999999659 ) ) ;
#50956=ORIENTED_EDGE ( 'NONE', *, *, #162726, .F. ) ;
#51026=CARTESIAN_POINT ( 'NONE',  ( -33.72168855820452649, 11.47316190337362940, -191.7499999999999716 ) ) ;
#51187=PLANE ( 'NONE',  #6919 ) ;
#51352=DIRECTION ( 'NONE',  ( 1.000000000000000000, 0.000000000000000000, 0.000000000000000000 ) ) ;
#51363=VERTEX_POINT ( 'NONE', #67377 ) ;
#51439=CARTESIAN_POINT ( 'NONE',  ( 12.25000000000000000, 9.350000000011140955, -184.2499999999999716 ) ) ;
#51507=LINE ( 'NONE', #230173, #245115 ) ;
#51651=DIRECTION ( 'NONE',  ( -1.000000000000000000, 0.000000000000000000, 0.000000000000000000 ) ) ;
#51778=CARTESIAN_POINT ( 'NONE',  ( -14.77538296656415184, 9.436662931810239741, -185.8230367322947814 ) ) ;
#51810=CIRCLE ( 'NONE', #97585, 1.500000000000001332 ) ;
#52091=EDGE_LOOP ( 'NONE', ( #208804, #230620, #84044, #174932 ) ) ;
#52146=ORIENTED_EDGE ( 'NONE', *, *, #62544, .F. ) ;
#52268=CARTESIAN_POINT ( 'NONE',  ( -16.84421487269769102, 9.950000000011135270, -180.1695021224448965 ) ) ;
#52366=ORIENTED_EDGE ( 'NONE', *, *, #39602, .T. ) ;
#52543=CARTESIAN_POINT ( 'NONE',  ( -17.71734398241073194, 10.84235722847571459, -190.7251382530055821 ) ) ;
#52575=ADVANCED_FACE ( 'NONE', ( #184792 ), #186086, .F. ) ;
#52579=DIRECTION ( 'NONE',  ( 0.000000000000000000, -1.000000000000000000, 0.000000000000000000 ) ) ;
#52832=CARTESIAN_POINT ( 'NONE',  ( -16.87036670365549895, 9.989418819312803066, -180.0204398826979286 ) ) ;
#52976=ORIENTED_EDGE ( 'NONE', *, *, #11742, .F. ) ;
#53064=ORIENTED_EDGE ( 'NONE', *, *, #128136, .T. ) ;
#53078=CARTESIAN_POINT ( 'NONE',  ( -12.30589683808040924, 9.356746017089406564, -184.7033597213641656 ) ) ;
#53322=ORIENTED_EDGE ( 'NONE', *, *, #222296, .F. ) ;
#53406=ORIENTED_EDGE ( 'NONE', *, *, #156226, .F. ) ;
#53432=DIRECTION ( 'NONE',  ( 1.000000000000000000, 0.000000000000000000, -0.000000000000000000 ) ) ;
#53452=EDGE_CURVE ( 'NONE', #433, #86347, #21062, .T. ) ;
#53509=AXIS2_PLACEMENT_3D ( 'NONE', #237031, #17966, #137907 ) ;
#53579=CARTESIAN_POINT ( 'NONE',  ( -16.97048326478264713, 9.950000000011137047, -180.6411068801271256 ) ) ;
#53694=ORIENTED_EDGE ( 'NONE', *, *, #91405, .F. ) ;
#53804=CARTESIAN_POINT ( 'NONE',  ( 18.39999999999999503, 5.650000000011139001, -191.7499999999999716 ) ) ;
#54006=CARTESIAN_POINT ( 'NONE',  ( -16.94445028196807002, 9.992063609708893068, -188.3926698215815350 ) ) ;
#54060=VERTEX_POINT ( 'NONE', #86790 ) ;
#54162=FACE_OUTER_BOUND ( 'NONE', #47675, .T. ) ;
#54201=CARTESIAN_POINT ( 'NONE',  ( 21.72449340488910607, 10.28395627750227703, -176.7499999999999716 ) ) ;
#54286=VECTOR ( 'NONE', #99447, 1000.000000000000000 ) ;
#54448=AXIS2_PLACEMENT_3D ( 'NONE', #210365, #112549, #173850 ) ;
#54454=DIRECTION ( 'NONE',  ( 0.000000000000000000, 1.000000000000000000, 0.000000000000000000 ) ) ;
#54575=LINE ( 'NONE', #55833, #108654 ) ;
#54711=PLANE ( 'NONE',  #86902 ) ;
#54867=AXIS2_PLACEMENT_3D ( 'NONE', #165119, #206812, #163839 ) ;
#54975=ORIENTED_EDGE ( 'NONE', *, *, #62544, .T. ) ;
#55013=CARTESIAN_POINT ( 'NONE',  ( -16.87435696428308063, 9.950002462943377424, -180.1499917651665328 ) ) ;
#55168=CARTESIAN_POINT ( 'NONE',  ( -17.11825945287481687, 10.05000000001113847, -188.3499999999999659 ) ) ;
#55200=CARTESIAN_POINT ( 'NONE',  ( 15.74999999999999645, 9.350000000011139178, -184.2499999999999716 ) ) ;
#55239=LINE ( 'NONE', #214351, #118894 ) ;
#55544=EDGE_CURVE ( 'NONE', #42862, #181967, #97442, .T. ) ;
#55800=EDGE_CURVE ( 'NONE', #86874, #195448, #175891, .T. ) ;
#55833=CARTESIAN_POINT ( 'NONE',  ( 18.39999999999999503, 11.47316190337363828, -180.1499999999999773 ) ) ;
#55863=CARTESIAN_POINT ( 'NONE',  ( -16.92778301347268766, 10.00094491684630604, -180.0714818920313860 ) ) ;
#55871=AXIS2_PLACEMENT_3D ( 'NONE', #232954, #73890, #193808 ) ;
#55954=CARTESIAN_POINT ( 'NONE',  ( -15.75000000000000355, 9.850000000011133849, -184.2499999999999716 ) ) ;
#55962=CARTESIAN_POINT ( 'NONE',  ( 18.54999999999999716, 8.750000000011173285, -180.1499999999999773 ) ) ;
#56287=EDGE_CURVE ( 'NONE', #169346, #58482, #66499, .T. ) ;
#56614=VERTEX_POINT ( 'NONE', #17429 ) ;
#56652=VERTEX_POINT ( 'NONE', #76116 ) ;
#56654=EDGE_CURVE ( 'NONE', #190492, #47603, #55239, .T. ) ;
#56892=ORIENTED_EDGE ( 'NONE', *, *, #32475, .F. ) ;
#57422=VERTEX_POINT ( 'NONE', #9761 ) ;
#57524=CARTESIAN_POINT ( 'NONE',  ( -16.94180778212363592, 9.992443055743303049, -180.1041835705331948 ) ) ;
#57589=CARTESIAN_POINT ( 'NONE',  ( -16.88560720703333473, 9.950564843760847822, -180.1481119208636983 ) ) ;
#57967=VECTOR ( 'NONE', #166345, 1000.000000000000000 ) ;
#58464=ORIENTED_EDGE ( 'NONE', *, *, #91405, .T. ) ;
#58482=VERTEX_POINT ( 'NONE', #98594 ) ;
#58684=CARTESIAN_POINT ( 'NONE',  ( -17.01825945287482966, 10.05000000001113847, -180.1499999999999773 ) ) ;
#58702=VECTOR ( 'NONE', #234137, 1000.000000000000000 ) ;
#58707=CARTESIAN_POINT ( 'NONE',  ( -16.89797118371800977, 9.976380722656529088, -188.4372933675600166 ) ) ;
#58777=CARTESIAN_POINT ( 'NONE',  ( 18.39999999999999503, 11.75000000001113953, -188.3499999999999659 ) ) ;
#58826=EDGE_LOOP ( 'NONE', ( #89905, #133014, #257254, #198901 ) ) ;
#58873=EDGE_CURVE ( 'NONE', #58482, #169346, #227146, .T. ) ;
#58894=ADVANCED_FACE ( 'NONE', ( #97008 ), #176609, .F. ) ;
#58946=CARTESIAN_POINT ( 'NONE',  ( 20.27550659511088682, 9.216043722520002035, -176.7499999999999716 ) ) ;
#59016=ORIENTED_EDGE ( 'NONE', *, *, #233725, .T. ) ;
#59177=EDGE_LOOP ( 'NONE', ( #7544, #102784, #209342, #102625, #88682, #216914, #62985, #198009, #62850, #185487, #145004, #31981 ) ) ;
#59379=VECTOR ( 'NONE', #99307, 1000.000000000000000 ) ;
#59443=DIRECTION ( 'NONE',  ( 1.000000000000000000, -0.000000000000000000, -0.000000000000000000 ) ) ;
#59898=CARTESIAN_POINT ( 'NONE',  ( -16.77683809663752257, 9.945835743215303282, -188.3360509808957488 ) ) ;
#59908=CARTESIAN_POINT ( 'NONE',  ( 15.39170923737819763, 9.389529397477893724, -185.3171079128936753 ) ) ;
#59978=DIRECTION ( 'NONE',  ( 1.000000000000000000, 0.000000000000000000, 0.000000000000000000 ) ) ;
#60096=CARTESIAN_POINT ( 'NONE',  ( -16.94445028196808778, 9.992063609708889516, -180.1073301784184366 ) ) ;
#60140=ADVANCED_FACE ( 'NONE', ( #8963 ), #70255, .F. ) ;
#60255=LINE ( 'NONE', #58946, #187746 ) ;
#60332=CARTESIAN_POINT ( 'NONE',  ( -17.01764560440361507, 9.950000000011138823, -188.2500000007888730 ) ) ;
#60473=CARTESIAN_POINT ( 'NONE',  ( -13.43673303185029688, 9.446648990640015953, -182.5891632959231288 ) ) ;
#60758=( NAMED_UNIT ( * ) PLANE_ANGLE_UNIT ( ) SI_UNIT ( $, .RADIAN. ) );
#61088=ORIENTED_EDGE ( 'NONE', *, *, #32475, .T. ) ;
#61218=CARTESIAN_POINT ( 'NONE',  ( 15.69410316191959254, 9.356746017089404788, -184.7033597213641656 ) ) ;
#61231=AXIS2_PLACEMENT_3D ( 'NONE', #27930, #109991, #67023 ) ;
#61285=ORIENTED_EDGE ( 'NONE', *, *, #194813, .T. ) ;
#61316=VECTOR ( 'NONE', #139373, 1000.000000000000000 ) ;
#61352=CARTESIAN_POINT ( 'NONE',  ( 20.73486653747088582, 7.250000000011182166, -176.7499999999999716 ) ) ;
#61395=CARTESIAN_POINT ( 'NONE',  ( -16.87683809663752754, 9.865889849342865503, -180.7674268070695121 ) ) ;
#61775=CARTESIAN_POINT ( 'NONE',  ( -13.12432614554022869, 9.430764995433474240, -182.7305373947504279 ) ) ;
#61987=CARTESIAN_POINT ( 'NONE',  ( 12.25000000000000000, 9.350000000011140955, -184.2499999999999716 ) ) ;
#62122=CARTESIAN_POINT ( 'NONE',  ( -23.25000000000000355, 9.950000000011138823, -176.7499999999999716 ) ) ;
#62229=CARTESIAN_POINT ( 'NONE',  ( -17.80356949364000130, 10.87673139701363745, -190.7130730242347738 ) ) ;
#62314=CARTESIAN_POINT ( 'NONE',  ( -16.94275863006528482, 9.989496048678669027, -188.3916973820765293 ) ) ;
#62409=( BOUNDED_SURFACE ( )  B_SPLINE_SURFACE ( 3, 2, ( 
 ( #252117, #70958, #87884 ),
 ( #167478, #147902, #227418 ),
 ( #60332, #238992, #139863 ),
 ( #155632, #255921, #55168 ) ),
 .UNSPECIFIED., .F., .F., .T. ) 
 B_SPLINE_SURFACE_WITH_KNOTS ( ( 4, 4 ),
 ( 3, 3 ),
 ( 3.658908243880901523, 4.712388980384689674 ),
 ( 0.000000000000000000, 1.000000000000000000 ),
 .UNSPECIFIED. ) 
 GEOMETRIC_REPRESENTATION_ITEM ( )  RATIONAL_B_SPLINE_SURFACE ( (
 ( 1.000000000000000000, 0.8984936768950646524, 1.000000000000000000),
 ( 1.000000000000000000, 0.8646876308616670004, 1.000000000000000000),
 ( 1.000000000000000000, 0.7953136715911841570, 1.000000000000000000),
 ( 1.000000000000000000, 0.7071067811866457165, 1.000000000000000000) ) ) 
 REPRESENTATION_ITEM ( '' )  SURFACE ( )  );
#62544=EDGE_CURVE ( 'NONE', #22307, #248393, #224554, .T. ) ;
#62568=LINE ( 'NONE', #58684, #219960 ) ;
#62580=ADVANCED_FACE ( 'NONE', ( #249277 ), #245425, .F. ) ;
#62688=CARTESIAN_POINT ( 'NONE',  ( -16.87683809663752399, 9.850000000011123191, -180.9023640181964652 ) ) ;
#62850=ORIENTED_EDGE ( 'NONE', *, *, #92779, .F. ) ;
#62861=PRODUCT_DEFINITION ( 'UNKNOWN', '', #232138, #254010 ) ;
#62911=AXIS2_PLACEMENT_3D ( 'NONE', #12838, #67650, #147186 ) ;
#62985=ORIENTED_EDGE ( 'NONE', *, *, #97611, .T. ) ;
#63203=EDGE_CURVE ( 'NONE', #86026, #22041, #69034, .T. ) ;
#63214=VECTOR ( 'NONE', #194329, 1000.000000000000000 ) ;
#63235=EDGE_CURVE ( 'NONE', #43046, #86026, #87932, .T. ) ;
#63435=FACE_OUTER_BOUND ( 'NONE', #128343, .T. ) ;
#63443=CARTESIAN_POINT ( 'NONE',  ( -18.40000000000000213, 11.47316190337364183, -191.6740539331919990 ) ) ;
#63455=ORIENTED_EDGE ( 'NONE', *, *, #84316, .T. ) ;
#63968=CARTESIAN_POINT ( 'NONE',  ( -16.97683809663752186, 9.950000000011137047, -180.9023640181964652 ) ) ;
#63988=FILL_AREA_STYLE ('',( #181393 ) ) ;
#64162=ORIENTED_EDGE ( 'NONE', *, *, #205184, .T. ) ;
#64232=ADVANCED_FACE ( 'NONE', ( #246142 ), #188724, .F. ) ;
#64540=CARTESIAN_POINT ( 'NONE',  ( 12.29592348164039883, 9.355806591641288250, -183.7911025315461302 ) ) ;
#65066=CARTESIAN_POINT ( 'NONE',  ( 13.77030915526559340, 9.456007326080465347, -185.9886334941467396 ) ) ;
#65146=CARTESIAN_POINT ( 'NONE',  ( -16.92209698673726237, 9.950000000011138823, -180.2106355670536573 ) ) ;
#65165=ORIENTED_EDGE ( 'NONE', *, *, #191849, .F. ) ;
#65264=( NAMED_UNIT ( * ) PLANE_ANGLE_UNIT ( ) SI_UNIT ( $, .RADIAN. ) );
#65658=ORIENTED_EDGE ( 'NONE', *, *, #31753, .T. ) ;
#65663=PLANE ( 'NONE',  #252713 ) ;
#65822=CARTESIAN_POINT ( 'NONE',  ( 15.74999999999999645, 9.350000000011139178, -184.0185689574026071 ) ) ;
#65918=AXIS2_PLACEMENT_3D ( 'NONE', #7465, #86977, #184816 ) ;
#65929=LINE ( 'NONE', #145448, #57967 ) ;
#65951=PLANE ( 'NONE',  #101703 ) ;
#65957=ORIENTED_EDGE ( 'NONE', *, *, #56287, .F. ) ;
#66080=( BOUNDED_CURVE ( )  B_SPLINE_CURVE ( 3, ( #37417, #19116, #2103, #238152 ),
 .UNSPECIFIED., .F., .F. ) 
 B_SPLINE_CURVE_WITH_KNOTS ( ( 4, 4 ),
 ( 4.712388980384689674, 5.672655318024514060 ),
 .UNSPECIFIED. ) 
 CURVE ( )  GEOMETRIC_REPRESENTATION_ITEM ( )  RATIONAL_B_SPLINE_CURVE ( ( 1.000000000000000000, 0.9246222802177627154, 0.9246222802177627154, 1.000000000000000000 ) ) 
 REPRESENTATION_ITEM ( '' )  );
#66377=LINE ( 'NONE', #207181, #11512 ) ;
#66499=B_SPLINE_CURVE_WITH_KNOTS ( 'NONE', 3,
 ( #131333, #110484, #70111, #53078, #250003, #50489, #132628, #10112, #190032, #111784, #107921, #187482, #93486, #11405, #29704, #191345, #90920, #51778, #12703, #109191, #92200, #173083, #13972, #227872, #171786, #71387, #150902, #230440, #212175, #167932 ),
 .UNSPECIFIED., .F., .F.,
 ( 4, 2, 2, 2, 2, 2, 2, 2, 2, 2, 2, 2, 2, 2, 4 ),
 ( 0.000000000000000000, 0.0003422764154113550820, 0.0006845528308227101641, 0.001026829246234065192, 0.001369105661645420328, 0.002053658492468071403, 0.002738211323290723129, 0.003080487738702051594, 0.003422764154113379625, 0.003765040569524708090, 0.004107316984936036121, 0.004449593400347364586, 0.004791869815758693051, 0.005134146231170021515, 0.005476422646581349113 ),
 .UNSPECIFIED. ) ;
#66794=EDGE_CURVE ( 'NONE', #231369, #100115, #210900, .T. ) ;
#66834=EDGE_LOOP ( 'NONE', ( #124155, #241344, #121680, #158151, #105958 ) ) ;
#66944=FACE_OUTER_BOUND ( 'NONE', #16231, .T. ) ;
#66960=CARTESIAN_POINT ( 'NONE',  ( -21.65000000000000213, 7.250000000011138646, -188.3499999999999659 ) ) ;
#67023=DIRECTION ( 'NONE',  ( -1.000000000000000000, 0.000000000000000000, 0.000000000000000000 ) ) ;
#67106=DIRECTION ( 'NONE',  ( 1.000000000000000000, 0.000000000000000000, 1.073024830501117725E-15 ) ) ;
#67377=CARTESIAN_POINT ( 'NONE',  ( 22.88900146558018989, 8.703904791123973084, -188.3499999999999659 ) ) ;
#67491=CARTESIAN_POINT ( 'NONE',  ( 18.39999999999999503, 5.650000000011139001, -180.1499999999999773 ) ) ;
#67546=EDGE_CURVE ( 'NONE', #25623, #96530, #143982, .T. ) ;
#67650=DIRECTION ( 'NONE',  ( 0.7071067811865493491, 0.7071067811865456854, 0.000000000000000000 ) ) ;
#67714=CIRCLE ( 'NONE', #250855, 0.09999999999998898659 ) ;
#67768=VERTEX_POINT ( 'NONE', #86561 ) ;
#67827=CARTESIAN_POINT ( 'NONE',  ( -18.38204789744325396, 11.47950103717623982, -191.7499999999999716 ) ) ;
#68026=FACE_OUTER_BOUND ( 'NONE', #81225, .T. ) ;
#68078=VECTOR ( 'NONE', #86038, 1000.000000000000000 ) ;
#68352=VERTEX_POINT ( 'NONE', #43014 ) ;
#68735=CARTESIAN_POINT ( 'NONE',  ( -16.89268316805465986, 9.951721813253337601, -188.3557524785454973 ) ) ;
#68774=CARTESIAN_POINT ( 'NONE',  ( -23.25000000000000355, 11.75000000001113953, -176.7499999999999716 ) ) ;
#68925=MECHANICAL_DESIGN_GEOMETRIC_PRESENTATION_REPRESENTATION('',(#23128),#135518);
#69034=B_SPLINE_CURVE_WITH_KNOTS ( 'NONE', 3,
 ( #61987, #25434, #64540, #82778, #202768, #24154, #224884, #81504, #205315, #184478, #85355, #101045, #5831, #244457, #46254, #219754, #22878, #103645, #7123, #159809, #141508, #183219, #239336, #164928, #65822, #144060 ),
 .UNSPECIFIED., .F., .F.,
 ( 4, 2, 2, 2, 2, 2, 2, 2, 2, 2, 2, 2, 4 ),
 ( 0.005476422646581339572, 0.006160811967703564394, 0.006845201288825788349, 0.007187395949386901628, 0.007529590609948013172, 0.007871785270509124716, 0.008213979931070237994, 0.008556174591631351273, 0.008898369252192462817, 0.009240563912753574360, 0.009582758573314687639, 0.01026714789443685175, 0.01095153721555902106 ),
 .UNSPECIFIED. ) ;
#69092=ADVANCED_FACE ( 'NONE', ( #17671 ), #257515, .T. ) ;
#69247=VECTOR ( 'NONE', #200921, 1000.000000000000000 ) ;
#69490=CARTESIAN_POINT ( 'NONE',  ( -16.85939591225059075, 9.905226478399006496, -180.4600682464689783 ) ) ;
#69499=B_SPLINE_CURVE_WITH_KNOTS ( 'NONE', 3,
 ( #182903, #48507, #22544, #4231, #204994, #143751, #104598, #105887, #223281, #124212 ),
 .UNSPECIFIED., .F., .F.,
 ( 4, 3, 3, 4 ),
 ( 0.000000000000000000, 4.874959354401679605E-05, 9.785140065121436244E-05, 0.0001360444631935818385 ),
 .UNSPECIFIED. ) ;
#69904=CARTESIAN_POINT ( 'NONE',  ( 12.60873083341397383, 9.389571634557567492, -185.3176407123691547 ) ) ;
#70111=CARTESIAN_POINT ( 'NONE',  ( -12.26136940704872025, 9.351403174152810749, -184.4795304368384734 ) ) ;
#70221=ORIENTED_EDGE ( 'NONE', *, *, #194813, .F. ) ;
#70255=PLANE ( 'NONE',  #62911 ) ;
#70318=CARTESIAN_POINT ( 'NONE',  ( -16.94445028196808778, 9.992063609708889516, -180.1073301784184366 ) ) ;
#70328=CARTESIAN_POINT ( 'NONE',  ( -16.91049119928364775, 9.950000000011138823, -180.1182796068091250 ) ) ;
#70428=ORIENTED_EDGE ( 'NONE', *, *, #183640, .F. ) ;
#70613=CARTESIAN_POINT ( 'NONE',  ( -18.39999999999999858, 11.47316190337362762, -176.8259460668079441 ) ) ;
#70774=DIRECTION ( 'NONE',  ( 0.2834754621636439431, -0.2834754621636535465, -0.9161240771326838450 ) ) ;
#70861=DIRECTION ( 'NONE',  ( 0.000000000000000000, -1.000000000000000000, 0.000000000000000000 ) ) ;
#70958=CARTESIAN_POINT ( 'NONE',  ( -16.91049119928363353, 9.950000000011137047, -188.3817203931907898 ) ) ;
#70988=DIRECTION ( 'NONE',  ( -1.073024830501117725E-15, 0.000000000000000000, 1.000000000000000000 ) ) ;
#71056=EDGE_CURVE ( 'NONE', #250008, #43046, #252455, .T. ) ;
#71159=VERTEX_POINT ( 'NONE', #143110 ) ;
#71216=LINE ( 'NONE', #150735, #14690 ) ;
#71387=CARTESIAN_POINT ( 'NONE',  ( -15.66061380678752180, 9.360723793997193454, -184.8139271946066913 ) ) ;
#71531=EDGE_CURVE ( 'NONE', #114189, #131422, #23753, .T. ) ;
#71809=LINE ( 'NONE', #50912, #23362 ) ;
#71814=CARTESIAN_POINT ( 'NONE',  ( 23.24999999999999645, 8.822561741677553471, -188.3499999999999659 ) ) ;
#71817=CARTESIAN_POINT ( 'NONE',  ( -18.40000000000000213, 5.650000000011139001, -180.1499999999999773 ) ) ;
#71887=EDGE_CURVE ( 'NONE', #86347, #131422, #21320, .T. ) ;
#71952=EDGE_LOOP ( 'NONE', ( #158001, #102993, #227804, #79500 ) ) ;
#72084=DIRECTION ( 'NONE',  ( 0.000000000000000000, -0.000000000000000000, -1.000000000000000000 ) ) ;
#72124=AXIS2_PLACEMENT_3D ( 'NONE', #246693, #224560, #48497 ) ;
#72251=PLANE ( 'NONE',  #151480 ) ;
#72549=FACE_OUTER_BOUND ( 'NONE', #25738, .T. ) ;
#72551=AXIS2_PLACEMENT_3D ( 'NONE', #154565, #20167, #197496 ) ;
#72747=DIRECTION ( 'NONE',  ( -0.000000000000000000, 0.000000000000000000, -1.000000000000000000 ) ) ;
#72958=DIRECTION ( 'NONE',  ( -1.000000000000000000, 3.854941057726231589E-15, 0.000000000000000000 ) ) ;
#73119=PLANE ( 'NONE',  #170208 ) ;
#73142=ORIENTED_EDGE ( 'NONE', *, *, #225705, .T. ) ;
#73277=ADVANCED_BREP_SHAPE_REPRESENTATION ( '', ( #191235, #2425 ), #131439 ) ;
#73291=ORIENTED_EDGE ( 'NONE', *, *, #164098, .T. ) ;
#73350=CARTESIAN_POINT ( 'NONE',  ( -16.87851181299898329, 9.950042924018893231, -180.1498564846330623 ) ) ;
#73367=CARTESIAN_POINT ( 'NONE',  ( -18.40000000000000213, 11.41458325961093756, -180.1499999999999488 ) ) ;
#73890=DIRECTION ( 'NONE',  ( 1.000000000000000000, -0.000000000000000000, -0.000000000000000000 ) ) ;
#73982=ADVANCED_FACE ( 'NONE', ( #92234 ), #120503, .F. ) ;
#74118=CARTESIAN_POINT ( 'NONE',  ( -21.64999999999999858, 10.05000000001113847, -188.3499999999999659 ) ) ;
#74392=CARTESIAN_POINT ( 'NONE',  ( -16.79363873026997922, 9.948850229429586634, -188.3461537814454516 ) ) ;
#74442=VECTOR ( 'NONE', #241215, 999.9999999999998863 ) ;
#74459=ADVANCED_FACE ( 'NONE', ( #135418 ), #154560, .T. ) ;
#74462=CARTESIAN_POINT ( 'NONE',  ( -16.92989143108098560, 9.950000000011138823, -180.3824838747567014 ) ) ;
#74524=ORIENTED_EDGE ( 'NONE', *, *, #124839, .F. ) ;
#74674=EDGE_LOOP ( 'NONE', ( #213041, #147718, #107570, #120824 ) ) ;
#74807=DIRECTION ( 'NONE',  ( 0.7071067811865463515, 0.7071067811865487940, 7.587431340288849180E-16 ) ) ;
#75092=LINE ( 'NONE', #54201, #89887 ) ;
#75216=AXIS2_PLACEMENT_3D ( 'NONE', #190133, #171882, #54454 ) ;
#75515=VERTEX_POINT ( 'NONE', #159483 ) ;
#75724=ORIENTED_EDGE ( 'NONE', *, *, #29266, .F. ) ;
#75836=CARTESIAN_POINT ( 'NONE',  ( -23.25000000000000355, 11.75000000001113953, -191.7499999999999716 ) ) ;
#75961=EDGE_CURVE ( 'NONE', #104626, #111385, #241295, .T. ) ;
#76014=ORIENTED_EDGE ( 'NONE', *, *, #55544, .F. ) ;
#76116=CARTESIAN_POINT ( 'NONE',  ( 21.13736287352038445, 8.046642376395153562, -188.3499999999999659 ) ) ;
#76286=ORIENTED_EDGE ( 'NONE', *, *, #40622, .T. ) ;
#76780=ORIENTED_EDGE ( 'NONE', *, *, #202746, .T. ) ;
#76915=SHAPE_DEFINITION_REPRESENTATION ( #128458, #206680 ) ;
#77005=CARTESIAN_POINT ( 'NONE',  ( -16.92570016628985030, 9.958788957751021798, -188.3793493299609452 ) ) ;
#77047=CARTESIAN_POINT ( 'NONE',  ( -21.64999999999999858, 9.350000000011133849, -176.7499999999999716 ) ) ;
#77069=EDGE_CURVE ( 'NONE', #244261, #243110, #166065, .T. ) ;
#77200=VERTEX_POINT ( 'NONE', #109489 ) ;
#77206=CARTESIAN_POINT ( 'NONE',  ( -16.87683809663752399, 9.865889849343231432, -187.7325731929304879 ) ) ;
#77473=APPLICATION_CONTEXT ( 'automotive_design' ) ;
#77672=EDGE_CURVE ( 'NONE', #86874, #141666, #10095, .T. ) ;
#77753=ORIENTED_EDGE ( 'NONE', *, *, #28259, .T. ) ;
#77803=ORIENTED_EDGE ( 'NONE', *, *, #5849, .F. ) ;
#77812=AXIS2_PLACEMENT_3D ( 'NONE', #30217, #210140, #126734 ) ;
#77830=EDGE_CURVE ( 'NONE', #86874, #165955, #211726, .T. ) ;
#77931=AXIS2_PLACEMENT_3D ( 'NONE', #91675, #9564, #70861 ) ;
#77938=CARTESIAN_POINT ( 'NONE',  ( 20.09999999999999787, 9.750000000011137757, -176.7499999999999716 ) ) ;
#78257=CARTESIAN_POINT ( 'NONE',  ( -16.89208623190940628, 9.951577948986638944, -188.3552722032182487 ) ) ;
#78285=DIRECTION ( 'NONE',  ( 0.000000000000000000, 0.000000000000000000, 1.000000000000000000 ) ) ;
#78333=ORIENTED_EDGE ( 'NONE', *, *, #4786, .T. ) ;
#78342=( BOUNDED_CURVE ( )  B_SPLINE_CURVE ( 3, ( #245457, #163348, #242872, #184172 ),
 .UNSPECIFIED., .F., .F. ) 
 B_SPLINE_CURVE_WITH_KNOTS ( ( 4, 4 ),
 ( 2.589852378279005940, 2.850972632318390598 ),
 .UNSPECIFIED. ) 
 CURVE ( )  GEOMETRIC_REPRESENTATION_ITEM ( )  RATIONAL_B_SPLINE_CURVE ( ( 1.000000000000000000, 0.9943260843901261525, 0.9943260843901261525, 1.000000000000000000 ) ) 
 REPRESENTATION_ITEM ( '' )  );
#78379=CARTESIAN_POINT ( 'NONE',  ( -16.93906926870270624, 10.01214687095770906, -180.0534523072267916 ) ) ;
#78382=CIRCLE ( 'NONE', #90856, 0.1999999999999987899 ) ;
#78444=CARTESIAN_POINT ( 'NONE',  ( -16.88815647973234135, 9.950832619326892114, -180.1472170633259680 ) ) ;
#78485=CARTESIAN_POINT ( 'NONE',  ( -16.97683810757273193, 9.950000000011137047, -187.7364232875387984 ) ) ;
#78537=LINE ( 'NONE', #158136, #92630 ) ;
#78752=CARTESIAN_POINT ( 'NONE',  ( -15.70407651835960650, 9.355806591641286474, -183.7911025315461018 ) ) ;
#79118=DIRECTION ( 'NONE',  ( -0.7071067811865562325, -0.7071067811865388020, 0.000000000000000000 ) ) ;
#79220=ORIENTED_EDGE ( 'NONE', *, *, #13690, .F. ) ;
#79360=CARTESIAN_POINT ( 'NONE',  ( -18.34374000495060386, 11.47316190337362585, -176.7499999999999716 ) ) ;
#79500=ORIENTED_EDGE ( 'NONE', *, *, #42233, .T. ) ;
#79501=B_SPLINE_CURVE_WITH_KNOTS ( 'NONE', 3,
 ( #233688, #176295, #78444, #57589, #135840, #73350, #234970, #55013, #155468, #193276 ),
 .UNSPECIFIED., .F., .F.,
 ( 4, 3, 3, 4 ),
 ( 1.950915401637565782E-15, 8.145022132839031210E-06, 1.905645951092651034E-05, 2.061107371226032482E-05 ),
 .UNSPECIFIED. ) ;
#79547=DIRECTION ( 'NONE',  ( 1.000000000000000000, 1.186688945009010077E-16, 0.000000000000000000 ) ) ;
#79593=DIRECTION ( 'NONE',  ( -1.020425574104004196E-15, 0.000000000000000000, 1.000000000000000000 ) ) ;
#79654=CARTESIAN_POINT ( 'NONE',  ( -16.93909480342659890, 9.993078364812696179, -180.1003470166722877 ) ) ;
#79756=CARTESIAN_POINT ( 'NONE',  ( -16.87998658237754768, 9.950000000011263168, -188.1363604322614833 ) ) ;
#79956=CARTESIAN_POINT ( 'NONE',  ( -16.93415306273742260, 9.995622260023671046, -188.4100569423603702 ) ) ;
#80016=CARTESIAN_POINT ( 'NONE',  ( -13.88555196119803448, 9.457431528860066550, -182.4999169378996555 ) ) ;
#80301=( LENGTH_UNIT ( ) NAMED_UNIT ( * ) SI_UNIT ( .MILLI., .METRE. ) );
#80461=CARTESIAN_POINT ( 'NONE',  ( -16.86578989773640913, 9.984809801269951990, -188.4646648866221881 ) ) ;
#80476=DIRECTION ( 'NONE',  ( -0.000000000000000000, -0.000000000000000000, -1.000000000000000000 ) ) ;
#80495=EDGE_LOOP ( 'NONE', ( #50956, #134979, #108834, #222915, #79220 ) ) ;
#80500=EDGE_CURVE ( 'NONE', #190492, #244261, #82903, .T. ) ;
#80645=B_SPLINE_CURVE_WITH_KNOTS ( 'NONE', 3,
 ( #88825, #91426, #53579, #189245, #74462, #207531, #171009, #191835, #52268, #172290 ),
 .UNSPECIFIED., .F., .F.,
 ( 4, 2, 2, 2, 4 ),
 ( 0.000000000000000000, 0.0003916577441626726262, 0.0005874866162440096169, 0.0006854010522846797114, 0.0007833154883253498060 ),
 .UNSPECIFIED. ) ;
#80652=LINE ( 'NONE', #18137, #132159 ) ;
#80756=EDGE_LOOP ( 'NONE', ( #76780, #143121, #114680, #19798 ) ) ;
#81156=CARTESIAN_POINT ( 'NONE',  ( -18.39999999999999858, 11.47316190337362762, -176.8259460668079441 ) ) ;
#81225=EDGE_LOOP ( 'NONE', ( #13029, #136282, #155353, #92607 ) ) ;
#81232=LINE ( 'NONE', #177818, #24526 ) ;
#81313=ORIENTED_EDGE ( 'NONE', *, *, #182684, .T. ) ;
#81504=CARTESIAN_POINT ( 'NONE',  ( 13.12220780326572367, 9.430633469083952392, -182.7317657948241276 ) ) ;
#81662=EDGE_LOOP ( 'NONE', ( #106784, #194674, #165851, #101039, #252488, #189808, #63455, #185208, #204092 ) ) ;
#81787=CARTESIAN_POINT ( 'NONE',  ( -23.25000000000000355, 5.650000000011139001, -176.7499999999999716 ) ) ;
#81991=VECTOR ( 'NONE', #2936, 1000.000000000000000 ) ;
#82133=EDGE_CURVE ( 'NONE', #179647, #154572, #245673, .T. ) ;
#82205=CARTESIAN_POINT ( 'NONE',  ( -16.97683810757273193, 9.950000000011137047, -180.7635767124612300 ) ) ;
#82584=CARTESIAN_POINT ( 'NONE',  ( -15.75000000000000355, 9.350000000011140955, -184.2499999999999716 ) ) ;
#82778=CARTESIAN_POINT ( 'NONE',  ( 12.47034474403012894, 9.375538102059163492, -183.3698758809907758 ) ) ;
#82797=DIRECTION ( 'NONE',  ( -0.000000000000000000, -0.000000000000000000, -1.000000000000000000 ) ) ;
#82903=( BOUNDED_CURVE ( )  B_SPLINE_CURVE ( 3, ( #63443, #8627, #24353, #103842 ),
 .UNSPECIFIED., .F., .F. ) 
 B_SPLINE_CURVE_WITH_KNOTS ( ( 4, 4 ),
 ( 5.733388419619902088, 5.983100554402347449 ),
 .UNSPECIFIED. ) 
 CURVE ( )  GEOMETRIC_REPRESENTATION_ITEM ( )  RATIONAL_B_SPLINE_CURVE ( ( 1.000000000000000000, 0.9948104011409417691, 0.9948104011409417691, 1.000000000000000000 ) ) 
 REPRESENTATION_ITEM ( '' )  );
#82976=CARTESIAN_POINT ( 'NONE',  ( 23.24999999999999645, 8.822561741677553471, -176.7499999999999716 ) ) ;
#83020=EDGE_CURVE ( 'NONE', #141666, #94057, #154639, .T. ) ;
#83031=CARTESIAN_POINT ( 'NONE',  ( -17.29838795457644807, 10.37154985795008599, -189.6047412826164020 ) ) ;
#83440=CARTESIAN_POINT ( 'NONE',  ( -18.40000000000000213, 11.48667500176882328, -176.7499999999999716 ) ) ;
#83490=CARTESIAN_POINT ( 'NONE',  ( -16.89155683852451162, 9.950000000011137047, -180.7773718495396622 ) ) ;
#83599=LINE ( 'NONE', #184015, #30133 ) ;
#83874=ORIENTED_EDGE ( 'NONE', *, *, #47642, .T. ) ;
#84044=ORIENTED_EDGE ( 'NONE', *, *, #103004, .F. ) ;
#84166=DIRECTION ( 'NONE',  ( 0.000000000000000000, 0.000000000000000000, 1.000000000000000000 ) ) ;
#84174=ORIENTED_EDGE ( 'NONE', *, *, #28259, .F. ) ;
#84192=ORIENTED_EDGE ( 'NONE', *, *, #75961, .F. ) ;
#84316=EDGE_CURVE ( 'NONE', #12552, #75515, #221350, .T. ) ;
#84370=EDGE_LOOP ( 'NONE', ( #152372, #233962, #227155, #218425, #88281, #131534, #207469, #230637, #32579, #32482, #188529, #196705, #53406, #88708 ) ) ;
#84466=CARTESIAN_POINT ( 'NONE',  ( -17.29838795458774570, 10.37154985796137296, -178.8952587173804716 ) ) ;
#84714=CARTESIAN_POINT ( 'NONE',  ( -18.35235881385853318, 11.47341900772405054, -176.7499999999999716 ) ) ;
#84717=CARTESIAN_POINT ( 'NONE',  ( -16.83199318825829494, 9.930646127992320160, -188.2275851882091615 ) ) ;
#84751=EDGE_CURVE ( 'NONE', #146114, #57422, #78342, .T. ) ;
#84760=CARTESIAN_POINT ( 'NONE',  ( -16.77977881697927032, 9.946601933544062746, -180.1613785731150017 ) ) ;
#84930=FACE_OUTER_BOUND ( 'NONE', #107401, .T. ) ;
#84991=ORIENTED_EDGE ( 'NONE', *, *, #126126, .T. ) ;
#85193=FACE_OUTER_BOUND ( 'NONE', #238110, .T. ) ;
#85355=CARTESIAN_POINT ( 'NONE',  ( 13.54556439290363912, 9.450592112144859058, -182.5561883188083527 ) ) ;
#85683=CARTESIAN_POINT ( 'NONE',  ( -16.90128866880175806, 9.953795777214113016, -188.3626761833886292 ) ) ;
#85759=CARTESIAN_POINT ( 'NONE',  ( -17.80356949364085040, 10.87673139701448299, -177.7869269757790676 ) ) ;
#85876=CARTESIAN_POINT ( 'NONE',  ( -15.55912972643740488, 8.490870273573721150, -188.3499999999999659 ) ) ;
#86026=VERTEX_POINT ( 'NONE', #51439 ) ;
#86038=DIRECTION ( 'NONE',  ( 0.000000000000000000, 0.000000000000000000, 1.000000000000000000 ) ) ;
#86065=EDGE_CURVE ( 'NONE', #46992, #220791, #18758, .T. ) ;
#86094=ORIENTED_EDGE ( 'NONE', *, *, #40615, .F. ) ;
#86117=CARTESIAN_POINT ( 'NONE',  ( 20.27550659511089037, 9.216043722520002035, -188.3499999999999659 ) ) ;
#86171=CARTESIAN_POINT ( 'NONE',  ( 18.54999999999999716, 8.750000000011182166, -188.3499999999999659 ) ) ;
#86224=DIRECTION ( 'NONE',  ( 0.000000000000000000, 0.000000000000000000, -1.000000000000000000 ) ) ;
#86294=FACE_OUTER_BOUND ( 'NONE', #166438, .T. ) ;
#86347=VERTEX_POINT ( 'NONE', #216330 ) ;
#86397=LINE ( 'NONE', #166003, #252619 ) ;
#86440=DIRECTION ( 'NONE',  ( 1.000000000000000000, 0.000000000000000000, 0.000000000000000000 ) ) ;
#86561=CARTESIAN_POINT ( 'NONE',  ( -18.40000000000000213, 11.47316190337362762, -180.0499999999999545 ) ) ;
#86756=AXIS2_PLACEMENT_3D ( 'NONE', #18791, #98296, #239137 ) ;
#86790=CARTESIAN_POINT ( 'NONE',  ( 18.54999999999999716, 9.950000000011153034, -180.1499999999999204 ) ) ;
#86874=VERTEX_POINT ( 'NONE', #197745 ) ;
#86902=AXIS2_PLACEMENT_3D ( 'NONE', #135515, #215070, #53432 ) ;
#86912=UNCERTAINTY_MEASURE_WITH_UNIT (LENGTH_MEASURE( 1.000000000000000082E-05 ), #166978, 'distance_accuracy_value', 'NONE');
#86977=DIRECTION ( 'NONE',  ( -1.000000000000000000, 0.000000000000000000, 0.000000000000000000 ) ) ;
#87025=AXIS2_PLACEMENT_3D ( 'NONE', #25228, #163440, #26509 ) ;
#87170=LINE ( 'NONE', #166763, #25821 ) ;
#87258=CARTESIAN_POINT ( 'NONE',  ( -16.90257928357874562, 9.954106821116520010, -180.1362854301136451 ) ) ;
#87309=CARTESIAN_POINT ( 'NONE',  ( -18.38639463286148867, 11.48019957384713230, -176.7499999999999716 ) ) ;
#87313=EDGE_CURVE ( 'NONE', #30570, #96530, #20103, .T. ) ;
#87475=CARTESIAN_POINT ( 'NONE',  ( -16.82542659449977762, 9.934499891438612451, -188.2553643999739847 ) ) ;
#87600=DIRECTION ( 'NONE',  ( -1.000000000000000000, 0.000000000000000000, 0.000000000000000000 ) ) ;
#87601=LINE ( 'NONE', #28983, #3074 ) ;
#87646=FACE_OUTER_BOUND ( 'NONE', #119883, .T. ) ;
#87727=CARTESIAN_POINT ( 'NONE',  ( -16.79139129368503802, 9.944944162472834748, -180.1702446328257849 ) ) ;
#87813=ORIENTED_EDGE ( 'NONE', *, *, #144447, .T. ) ;
#87884=CARTESIAN_POINT ( 'NONE',  ( -16.93388492042257809, 9.988541822527057690, -188.4005451231861628 ) ) ;
#87932=LINE ( 'NONE', #249616, #226273 ) ;
#88281=ORIENTED_EDGE ( 'NONE', *, *, #87313, .T. ) ;
#88488=EDGE_CURVE ( 'NONE', #224829, #2708, #245607, .T. ) ;
#88672=DIRECTION ( 'NONE',  ( -0.000000000000000000, 1.000000000000000000, -0.000000000000000000 ) ) ;
#88682=ORIENTED_EDGE ( 'NONE', *, *, #87313, .F. ) ;
#88702=CIRCLE ( 'NONE', #92805, 0.9000000000000014655 ) ;
#88708=ORIENTED_EDGE ( 'NONE', *, *, #25549, .F. ) ;
#88751=CARTESIAN_POINT ( 'NONE',  ( -16.83558968593874638, 9.950000000011137047, -188.3376948123832619 ) ) ;
#88825=CARTESIAN_POINT ( 'NONE',  ( -16.97683809663752186, 9.950000000011138823, -180.9023640181964652 ) ) ;
#88967=CARTESIAN_POINT ( 'NONE',  ( -14.00000000000000178, 9.850000000011133849, -184.2499999999999716 ) ) ;
#89315=DIRECTION ( 'NONE',  ( 0.5932847527679310229, -0.8049926720990042694, 0.000000000000000000 ) ) ;
#89425=CARTESIAN_POINT ( 'NONE',  ( -18.40000000000000213, 11.33174054713633261, -188.3499999999999659 ) ) ;
#89566=LINE ( 'NONE', #223940, #172992 ) ;
#89830=CARTESIAN_POINT ( 'NONE',  ( -16.89268316805466341, 9.951721813253341153, -180.1442475214544174 ) ) ;
#89887=VECTOR ( 'NONE', #210719, 1000.000000000000000 ) ;
#89903=CARTESIAN_POINT ( 'NONE',  ( 20.99999999999999645, 9.750000000011137757, -180.1499999999999773 ) ) ;
#89905=ORIENTED_EDGE ( 'NONE', *, *, #205750, .F. ) ;
#89921=ORIENTED_EDGE ( 'NONE', *, *, #233725, .F. ) ;
#90113=DIRECTION ( 'NONE',  ( -1.073024830501117725E-15, -0.000000000000000000, -1.000000000000000000 ) ) ;
#90116=EDGE_LOOP ( 'NONE', ( #45472, #39058, #154432, #237649 ) ) ;
#90297=CARTESIAN_POINT ( 'NONE',  ( -16.87372386987899020, 9.880600233647918174, -180.6492698718663519 ) ) ;
#90560=CARTESIAN_POINT ( 'NONE',  ( -16.93658211146646408, 9.994108662352344297, -180.0957049300442918 ) ) ;
#90692=VECTOR ( 'NONE', #191004, 1000.000000000000000 ) ;
#90713=CARTESIAN_POINT ( 'NONE',  ( 12.25000000000000355, 9.350000000011142731, -184.3642676076160569 ) ) ;
#90856=AXIS2_PLACEMENT_3D ( 'NONE', #136198, #20152, #38420 ) ;
#90920=CARTESIAN_POINT ( 'NONE',  ( -14.56336952470180002, 9.446645344706398717, -185.9108064561001470 ) ) ;
#91032=AXIS2_PLACEMENT_3D ( 'NONE', #160396, #42997, #3862 ) ;
#91240=CARTESIAN_POINT ( 'NONE',  ( -16.84981964351498007, 9.917318234109993469, -180.3696016140194445 ) ) ;
#91256=CARTESIAN_POINT ( 'NONE',  ( -18.40000000000000213, 11.48667500176882861, -191.7499999999999716 ) ) ;
#91405=EDGE_CURVE ( 'NONE', #22307, #111909, #44854, .T. ) ;
#91426=CARTESIAN_POINT ( 'NONE',  ( -16.97683809663752896, 9.950000000011140600, -180.7715247686699627 ) ) ;
#91675=CARTESIAN_POINT ( 'NONE',  ( -21.64999999999999858, 10.05000000001113847, -180.2499999999999716 ) ) ;
#91873=CARTESIAN_POINT ( 'NONE',  ( -12.25000000000000178, 9.850000000011133849, -184.2499999999999716 ) ) ;
#92002=CARTESIAN_POINT ( 'NONE',  ( 12.30626653967340900, 9.356790025057033944, -184.7048265086138201 ) ) ;
#92168=CARTESIAN_POINT ( 'NONE',  ( 20.73486653747088937, 7.750000000011182166, -188.3499999999999659 ) ) ;
#92200=CARTESIAN_POINT ( 'NONE',  ( -15.15564720441980029, 9.410708747058235346, -185.5692084058440798 ) ) ;
#92234=FACE_OUTER_BOUND ( 'NONE', #245103, .T. ) ;
#92502=CARTESIAN_POINT ( 'NONE',  ( -16.82542659449978117, 9.934499891438612451, -180.2446356000259868 ) ) ;
#92578=CARTESIAN_POINT ( 'NONE',  ( -16.89021194854739605, 9.950000000011137047, -188.2425681316042585 ) ) ;
#92607=ORIENTED_EDGE ( 'NONE', *, *, #77069, .F. ) ;
#92630=VECTOR ( 'NONE', #197207, 1000.000000000000000 ) ;
#92779=EDGE_CURVE ( 'NONE', #75515, #171571, #101512, .T. ) ;
#92805=AXIS2_PLACEMENT_3D ( 'NONE', #200609, #201892, #237176 ) ;
#92964=CARTESIAN_POINT ( 'NONE',  ( 17.23472005113826810, 10.30788195451192202, -189.5465768600686545 ) ) ;
#92969=CARTESIAN_POINT ( 'NONE',  ( 20.05000000000002913, 7.250000000011171508, -176.7499999999999716 ) ) ;
#93039=CARTESIAN_POINT ( 'NONE',  ( 15.48841904831874849, 8.561580951692381092, -188.3499999999999659 ) ) ;
#93295=DIRECTION ( 'NONE',  ( -0.000000000000000000, -0.000000000000000000, -1.000000000000000000 ) ) ;
#93406=CYLINDRICAL_SURFACE ( 'NONE', #55871, 14.30833333333333890 ) ;
#93486=CARTESIAN_POINT ( 'NONE',  ( -13.77083647240106679, 9.457410930301319851, -185.9999159087463170 ) ) ;
#93981=CARTESIAN_POINT ( 'NONE',  ( -18.40000000000000213, 11.47316190337364183, -188.4499999999999886 ) ) ;
#94057=VERTEX_POINT ( 'NONE', #86171 ) ;
#94147=DIRECTION ( 'NONE',  ( 0.000000000000000000, 0.9553114395363172529, -0.2956011730204217702 ) ) ;
#94168=CARTESIAN_POINT ( 'NONE',  ( -18.40000000000000213, 11.47316190337362940, -180.1085786437626552 ) ) ;
#94610=AXIS2_PLACEMENT_3D ( 'NONE', #246725, #125504, #189341 ) ;
#94611=VECTOR ( 'NONE', #240352, 1000.000000000000000 ) ;
#94643=DIRECTION ( 'NONE',  ( -1.073024830501117725E-15, 0.000000000000000000, 1.000000000000000000 ) ) ;
#94676=ORIENTED_EDGE ( 'NONE', *, *, #67546, .F. ) ;
#94747=EDGE_LOOP ( 'NONE', ( #74524, #76286, #222974, #2399, #193531, #171626, #70428, #43836, #163605 ) ) ;
#95220=CARTESIAN_POINT ( 'NONE',  ( -15.75000000000000355, 9.850000000011133849, -184.2499999999999716 ) ) ;
#95268=CARTESIAN_POINT ( 'NONE',  ( -17.11825945287482753, 10.05000000001113847, -180.1499999999999773 ) ) ;
#95389=CARTESIAN_POINT ( 'NONE',  ( -16.93772744219066340, 9.993541108763512426, -180.0980619719696847 ) ) ;
#95704=CARTESIAN_POINT ( 'NONE',  ( 18.39999999999999503, 11.47316190337363828, -188.3499999999999659 ) ) ;
#96265=ORIENTED_EDGE ( 'NONE', *, *, #20948, .T. ) ;
#96284=CARTESIAN_POINT ( 'NONE',  ( -16.89797118371585682, 9.976380722655704858, -180.0627066324412340 ) ) ;
#96462=PRODUCT_CONTEXT ( 'NONE', #39080, 'mechanical' ) ;
#96530=VERTEX_POINT ( 'NONE', #241303 ) ;
#96549=CARTESIAN_POINT ( 'NONE',  ( -16.85718274719488363, 9.976142314632912900, -188.4366536678175521 ) ) ;
#96588=FACE_OUTER_BOUND ( 'NONE', #11871, .T. ) ;
#96637=CARTESIAN_POINT ( 'NONE',  ( -16.93970660449832977, 10.01284139164673270, -180.0522817357944234 ) ) ;
#96748=CARTESIAN_POINT ( 'NONE',  ( -16.87683809663752399, 9.950000000011137047, -187.5976359818036485 ) ) ;
#96792=DIRECTION ( 'NONE',  ( -0.000000000000000000, -0.000000000000000000, -1.000000000000000000 ) ) ;
#96833=AXIS2_PLACEMENT_3D ( 'NONE', #198240, #97830, #78285 ) ;
#96987=B_SPLINE_CURVE_WITH_KNOTS ( 'NONE', 3,
 ( #48196, #45641, #125181, #9074, #247686, #148598, #84717, #228134, #49488, #185145, #129032, #208581, #189001, #10376 ),
 .UNSPECIFIED., .F., .F.,
 ( 4, 2, 2, 2, 2, 2, 4 ),
 ( 2.797157557069881010E-17, 0.0003823333598417795291, 0.0005735000397626551991, 0.0006690833797230931424, 0.0007168750497033133610, 0.0007407708846934235244, 0.0007646667196835337963 ),
 .UNSPECIFIED. ) ;
#97008=FACE_OUTER_BOUND ( 'NONE', #192553, .T. ) ;
#97139=CARTESIAN_POINT ( 'NONE',  ( -21.65000000000000213, 9.950000000011138823, -180.2499999999999716 ) ) ;
#97172=DIRECTION ( 'NONE',  ( -1.000000000000000000, 0.000000000000000000, 0.000000000000000000 ) ) ;
#97250=ORIENTED_EDGE ( 'NONE', *, *, #182493, .T. ) ;
#97288=CARTESIAN_POINT ( 'NONE',  ( -33.72168855820451938, 9.950000000011156587, -188.3500000000000227 ) ) ;
#97423=ORIENTED_EDGE ( 'NONE', *, *, #53452, .T. ) ;
#97442=CIRCLE ( 'NONE', #72551, 0.1999999999999987899 ) ;
#97554=CARTESIAN_POINT ( 'NONE',  ( -16.90202395485789211, 9.965944544561791574, -180.0969862787400473 ) ) ;
#97585=AXIS2_PLACEMENT_3D ( 'NONE', #31479, #90113, #49723 ) ;
#97611=EDGE_CURVE ( 'NONE', #239382, #43357, #254442, .T. ) ;
#97732=CARTESIAN_POINT ( 'NONE',  ( -16.78270389226384651, 9.947372616628161524, -188.3412070369114417 ) ) ;
#97830=DIRECTION ( 'NONE',  ( -0.7071067811865487940, 0.7071067811865463515, 0.000000000000000000 ) ) ;
#97922=CARTESIAN_POINT ( 'NONE',  ( 23.04999999999999716, 8.822561741677553471, -176.7499999999999716 ) ) ;
#98097=EDGE_CURVE ( 'NONE', #235554, #10681, #88702, .T. ) ;
#98296=DIRECTION ( 'NONE',  ( -0.000000000000000000, -0.000000000000000000, -1.000000000000000000 ) ) ;
#98542=ADVANCED_FACE ( 'NONE', ( #140298 ), #197720, .F. ) ;
#98594=CARTESIAN_POINT ( 'NONE',  ( -15.75000000000000355, 9.350000000011140955, -184.2499999999999716 ) ) ;
#98660=CYLINDRICAL_SURFACE ( 'NONE', #250835, 0.1000000000000013656 ) ;
#98742=CARTESIAN_POINT ( 'NONE',  ( -16.87786941232801396, 9.958154714156124854, -188.3771857997939492 ) ) ;
#98831=CARTESIAN_POINT ( 'NONE',  ( -16.94333152882356330, 9.990342011468825945, -188.3920315311014519 ) ) ;
#99307=DIRECTION ( 'NONE',  ( -1.020425574104004196E-15, -0.000000000000000000, -1.000000000000000000 ) ) ;
#99321=CARTESIAN_POINT ( 'NONE',  ( -16.93710578446422588, 9.950000000011137047, -188.0811960162001526 ) ) ;
#99447=DIRECTION ( 'NONE',  ( 0.5932847527679310229, -0.8049926720990042694, -6.366092712777067056E-16 ) ) ;
#99586=CARTESIAN_POINT ( 'NONE',  ( -14.45443560709636088, 9.450592112144859058, -182.5561883188083812 ) ) ;
#99594=CARTESIAN_POINT ( 'NONE',  ( 18.39999999999999503, 11.75000000001113953, -188.3499999999999659 ) ) ;
#99638=ADVANCED_FACE ( 'NONE', ( #142906 ), #221170, .T. ) ;
#100115=VERTEX_POINT ( 'NONE', #1811 ) ;
#100124=CARTESIAN_POINT ( 'NONE',  ( -16.89318236219976299, 9.951535257886295227, -180.1448703678941001 ) ) ;
#100195=CARTESIAN_POINT ( 'NONE',  ( -20.65000000000000568, 7.250000000011138646, -188.3499999999999659 ) ) ;
#100198=CARTESIAN_POINT ( 'NONE',  ( -17.22767730082392745, 10.34924421247985471, -178.8575713094251967 ) ) ;
#100616=ORIENTED_EDGE ( 'NONE', *, *, #182493, .F. ) ;
#100642=EDGE_CURVE ( 'NONE', #22041, #86026, #222433, .T. ) ;
#100828=LINE ( 'NONE', #180420, #249138 ) ;
#101039=ORIENTED_EDGE ( 'NONE', *, *, #88488, .F. ) ;
#101045=CARTESIAN_POINT ( 'NONE',  ( 13.76927104934457802, 9.455987233623901034, -182.5115311668978393 ) ) ;
#101056=( BOUNDED_CURVE ( )  B_SPLINE_CURVE ( 3, ( #182871, #238979, #159445, #81156 ),
 .UNSPECIFIED., .F., .F. ) 
 B_SPLINE_CURVE_WITH_KNOTS ( ( 4, 4 ),
 ( 0.3000847527772381729, 0.5497968875596822569 ),
 .UNSPECIFIED. ) 
 CURVE ( )  GEOMETRIC_REPRESENTATION_ITEM ( )  RATIONAL_B_SPLINE_CURVE ( ( 1.000000000000000000, 0.9948104011409419911, 0.9948104011409419911, 1.000000000000000000 ) ) 
 REPRESENTATION_ITEM ( '' )  );
#101126=( NAMED_UNIT ( * ) SI_UNIT ( $, .STERADIAN. ) SOLID_ANGLE_UNIT ( ) );
#101290=CARTESIAN_POINT ( 'NONE',  ( -16.91256925476568540, 9.985731158139326880, -188.4676424890052431 ) ) ;
#101512=LINE ( 'NONE', #221476, #61316 ) ;
#101703=AXIS2_PLACEMENT_3D ( 'NONE', #185891, #84166, #240744 ) ;
#101768=CARTESIAN_POINT ( 'NONE',  ( -16.85697194749123540, 9.908543714134728120, -180.4350042676138060 ) ) ;
#101938=EDGE_LOOP ( 'NONE', ( #59016, #27194 ) ) ;
#101963=ORIENTED_EDGE ( 'NONE', *, *, #14011, .F. ) ;
#102150=CARTESIAN_POINT ( 'NONE',  ( -13.54795643572458097, 9.450668889178684751, -182.5555464902073197 ) ) ;
#102330=ORIENTED_EDGE ( 'NONE', *, *, #13753, .T. ) ;
#102515=CARTESIAN_POINT ( 'NONE',  ( -15.55912972643740488, 8.490870273573721150, -188.4499999999999886 ) ) ;
#102625=ORIENTED_EDGE ( 'NONE', *, *, #67546, .T. ) ;
#102664=ADVANCED_FACE ( 'NONE', ( #68026 ), #8313, .T. ) ;
#102784=ORIENTED_EDGE ( 'NONE', *, *, #29649, .F. ) ;
#102951=CARTESIAN_POINT ( 'NONE',  ( -14.00000000000000178, 9.850000000011133849, -184.2499999999999716 ) ) ;
#102960=DIRECTION ( 'NONE',  ( 1.186688945009009831E-16, -1.000000000000000000, 0.000000000000000000 ) ) ;
#102993=ORIENTED_EDGE ( 'NONE', *, *, #84316, .F. ) ;
#103004=EDGE_CURVE ( 'NONE', #192577, #257956, #131437, .T. ) ;
#103182=ORIENTED_EDGE ( 'NONE', *, *, #6043, .F. ) ;
#103313=CARTESIAN_POINT ( 'NONE',  ( -17.11825945287482753, 9.950000000011138823, -180.2499999999999716 ) ) ;
#103645=CARTESIAN_POINT ( 'NONE',  ( 14.77516762759921853, 9.436674251854007878, -182.6768619309992800 ) ) ;
#103719=SURFACE_SIDE_STYLE ('',( #2064 ) ) ;
#103834=CYLINDRICAL_SURFACE ( 'NONE', #54867, 1.749999999999999778 ) ;
#103842=CARTESIAN_POINT ( 'NONE',  ( -16.94107738177414291, 10.01423928514777373, -188.4499999999999886 ) ) ;
#104015=DIRECTION ( 'NONE',  ( -1.000000000000000000, -0.000000000000000000, -0.000000000000000000 ) ) ;
#104052=DIRECTION ( 'NONE',  ( 0.000000000000000000, -0.9553114395363172529, -0.2956011730204217702 ) ) ;
#104312=ORIENTED_EDGE ( 'NONE', *, *, #88488, .T. ) ;
#104587=LINE ( 'NONE', #184146, #81991 ) ;
#104598=CARTESIAN_POINT ( 'NONE',  ( -16.87368910959167678, 9.961273816702552963, -180.1124930966405771 ) ) ;
#104607=ORIENTED_EDGE ( 'NONE', *, *, #248993, .T. ) ;
#104626=VERTEX_POINT ( 'NONE', #216923 ) ;
#105170=VECTOR ( 'NONE', #37075, 1000.000000000000000 ) ;
#105194=EDGE_CURVE ( 'NONE', #189000, #46992, #146071, .T. ) ;
#105229=CARTESIAN_POINT ( 'NONE',  ( 18.54999999999999716, 8.750000000011182166, -176.7499999999999716 ) ) ;
#105376=CARTESIAN_POINT ( 'NONE',  ( 21.13736287352038445, 8.046642376395153562, -176.7499999999999716 ) ) ;
#105567=EDGE_CURVE ( 'NONE', #136660, #224829, #187162, .T. ) ;
#105617=CARTESIAN_POINT ( 'NONE',  ( -16.81744102076749314, 9.950000000011142376, -180.1499999999999773 ) ) ;
#105738=CARTESIAN_POINT ( 'NONE',  ( -16.84793658983412712, 9.950000000011073098, -188.2663533221895591 ) ) ;
#105887=CARTESIAN_POINT ( 'NONE',  ( -16.87845715379269507, 9.957858113908169884, -180.1238006510588718 ) ) ;
#105958=ORIENTED_EDGE ( 'NONE', *, *, #20925, .T. ) ;
#106010=CARTESIAN_POINT ( 'NONE',  ( 13.99999999999999822, 9.850000000011137402, -184.2499999999999716 ) ) ;
#106784=ORIENTED_EDGE ( 'NONE', *, *, #11742, .T. ) ;
#106841=ORIENTED_EDGE ( 'NONE', *, *, #49144, .T. ) ;
#106922=AXIS2_PLACEMENT_3D ( 'NONE', #106010, #123042, #86440 ) ;
#106925=CIRCLE ( 'NONE', #181948, 0.09999999999999602263 ) ;
#107112=EDGE_CURVE ( 'NONE', #250008, #22041, #51507, .T. ) ;
#107170=DIRECTION ( 'NONE',  ( 1.020425574104004196E-15, 1.210927747993693964E-31, -1.000000000000000000 ) ) ;
#107401=EDGE_LOOP ( 'NONE', ( #30476, #224991, #249653, #47400 ) ) ;
#107570=ORIENTED_EDGE ( 'NONE', *, *, #126284, .T. ) ;
#107596=VERTEX_POINT ( 'NONE', #208364 ) ;
#107681=DIRECTION ( 'NONE',  ( 0.7071067811865487940, 0.7071067811865462405, -7.215498431451186046E-16 ) ) ;
#107775=CARTESIAN_POINT ( 'NONE',  ( -20.65000000000000568, 5.650000000011139001, -188.3499999999999659 ) ) ;
#107921=CARTESIAN_POINT ( 'NONE',  ( -13.11924609551136101, 9.431689550535258704, -185.7792900322359912 ) ) ;
#108043=DIRECTION ( 'NONE',  ( 0.000000000000000000, -1.000000000000000000, 0.000000000000000000 ) ) ;
#108080=DIRECTION ( 'NONE',  ( 1.000000000000000000, 0.000000000000000000, 0.000000000000000000 ) ) ;
#108131=CARTESIAN_POINT ( 'NONE',  ( -16.91247567987037570, 9.959082683680401615, -180.1287244585373060 ) ) ;
#108144=ORIENTED_EDGE ( 'NONE', *, *, #77830, .F. ) ;
#108349=CARTESIAN_POINT ( 'NONE',  ( -16.77431908686106610, 9.945805754529134290, -188.3358392176502036 ) ) ;
#108398=ADVANCED_FACE ( 'NONE', ( #229860 ), #51187, .F. ) ;
#108576=VERTEX_POINT ( 'NONE', #220261 ) ;
#108630=ORIENTED_EDGE ( 'NONE', *, *, #103004, .T. ) ;
#108654=VECTOR ( 'NONE', #107170, 1000.000000000000000 ) ;
#108798=DIRECTION ( 'NONE',  ( 1.186688945009010077E-16, -1.000000000000000000, -0.000000000000000000 ) ) ;
#108834=ORIENTED_EDGE ( 'NONE', *, *, #257479, .T. ) ;
#108986=CARTESIAN_POINT ( 'NONE',  ( -18.40000000000000213, 11.47316190337364183, -188.3914213562372311 ) ) ;
#109017=ORIENTED_EDGE ( 'NONE', *, *, #27587, .T. ) ;
#109057=ADVANCED_FACE ( 'NONE', ( #47697 ), #28185, .F. ) ;
#109082=PLANE ( 'NONE',  #177108 ) ;
#109182=ORIENTED_EDGE ( 'NONE', *, *, #202746, .F. ) ;
#109191=CARTESIAN_POINT ( 'NONE',  ( -15.06720934482786234, 9.417690691074259490, -185.6416006967645274 ) ) ;
#109347=VECTOR ( 'NONE', #74807, 999.9999999999998863 ) ;
#109384=EDGE_CURVE ( 'NONE', #51363, #247233, #78382, .T. ) ;
#109489=CARTESIAN_POINT ( 'NONE',  ( 21.13736287352038445, 8.046642376395153562, -180.1499999999999773 ) ) ;
#109511=CARTESIAN_POINT ( 'NONE',  ( -18.38817693311004575, 11.48149151591092476, -191.7499999999999716 ) ) ;
#109570=DIRECTION ( 'NONE',  ( -0.7071067811865487940, 0.7071067811865463515, -7.215498431451184074E-16 ) ) ;
#109780=CYLINDRICAL_SURFACE ( 'NONE', #94610, 0.5000000000000004441 ) ;
#109862=CARTESIAN_POINT ( 'NONE',  ( -16.77683809663752257, 9.945835743215301505, -180.1639490191041943 ) ) ;
#109934=ADVANCED_FACE ( 'NONE', ( #251718 ), #73119, .F. ) ;
#109968=ORIENTED_EDGE ( 'NONE', *, *, #55544, .T. ) ;
#109991=DIRECTION ( 'NONE',  ( 1.073024830501117725E-15, 0.000000000000000000, 1.000000000000000000 ) ) ;
#110042=FACE_OUTER_BOUND ( 'NONE', #66834, .T. ) ;
#110073=DIRECTION ( 'NONE',  ( 0.000000000000000000, 0.000000000000000000, -1.000000000000000000 ) ) ;
#110484=CARTESIAN_POINT ( 'NONE',  ( -12.25000000000000000, 9.350000000011132073, -184.3657431672738767 ) ) ;
#110692=CARTESIAN_POINT ( 'NONE',  ( -16.94389599338512298, 9.991197989766199328, -180.1076448018102099 ) ) ;
#110708=CARTESIAN_POINT ( 'NONE',  ( -17.01473183483382812, 9.950000000011137047, -180.2499999999999716 ) ) ;
#110786=CARTESIAN_POINT ( 'NONE',  ( -16.79270642812298320, 9.946244216949343908, -180.1610667214370665 ) ) ;
#110908=CARTESIAN_POINT ( 'NONE',  ( 22.88900146558018989, 8.703904791123973084, -176.7499999999999716 ) ) ;
#111385=VERTEX_POINT ( 'NONE', #152568 ) ;
#111415=ADVANCED_FACE ( 'NONE', ( #33922 ), #54711, .F. ) ;
#111578=CARTESIAN_POINT ( 'NONE',  ( 13.12229106158772751, 9.430637101707896264, -185.7682606180609639 ) ) ;
#111690=ORIENTED_EDGE ( 'NONE', *, *, #137107, .F. ) ;
#111712=DIRECTION ( 'NONE',  ( -0.000000000000000000, 1.000000000000000000, -0.000000000000000000 ) ) ;
#111763=ORIENTED_EDGE ( 'NONE', *, *, #13753, .F. ) ;
#111784=CARTESIAN_POINT ( 'NONE',  ( -12.92414019175886786, 9.417632963117448242, -185.6489484657322464 ) ) ;
#111816=ORIENTED_EDGE ( 'NONE', *, *, #71056, .T. ) ;
#111909=VERTEX_POINT ( 'NONE', #249422 ) ;
#112097=CARTESIAN_POINT ( 'NONE',  ( -16.87998658237742333, 9.950000000011138823, -180.3636395677385167 ) ) ;
#112337=DIRECTION ( 'NONE',  ( 1.000000000000000000, -0.000000000000000000, -0.000000000000000000 ) ) ;
#112358=AXIS2_PLACEMENT_3D ( 'NONE', #41613, #24623, #2442 ) ;
#112549=DIRECTION ( 'NONE',  ( 0.7071067811865463515, -0.7071067811865487940, 0.000000000000000000 ) ) ;
#112805=CARTESIAN_POINT ( 'NONE',  ( -21.65000000000000213, 7.250000000011139534, -180.1499999999999773 ) ) ;
#112827=DIRECTION ( 'NONE',  ( 0.000000000000000000, 0.000000000000000000, -1.000000000000000000 ) ) ;
#112988=FACE_BOUND ( 'NONE', #208620, .T. ) ;
#113216=EDGE_CURVE ( 'NONE', #165955, #195448, #114097, .T. ) ;
#113252=DIRECTION ( 'NONE',  ( 0.7071067811865463515, -0.7071067811865487940, 4.930380657631324879E-32 ) ) ;
#113440=CARTESIAN_POINT ( 'NONE',  ( -16.84419801905645997, 9.950000000011140600, -188.3305101537779080 ) ) ;
#114097=LINE ( 'NONE', #37159, #179631 ) ;
#114189=VERTEX_POINT ( 'NONE', #206832 ) ;
#114437=ADVANCED_FACE ( 'NONE', ( #232835 ), #132433, .T. ) ;
#114680=ORIENTED_EDGE ( 'NONE', *, *, #183746, .F. ) ;
#114952=CARTESIAN_POINT ( 'NONE',  ( -16.94309007106720699, 9.992226192581142641, -180.1057912825554581 ) ) ;
#115267=CARTESIAN_POINT ( 'NONE',  ( -16.93658211146644987, 9.994108662352344297, -188.4042950699556513 ) ) ;
#115419=CARTESIAN_POINT ( 'NONE',  ( 20.99999999999999645, 9.750000000011137757, -176.7499999999999716 ) ) ;
#115424=CIRCLE ( 'NONE', #15506, 0.09999999999999602263 ) ;
#115874=ORIENTED_EDGE ( 'NONE', *, *, #29386, .F. ) ;
#116142=CARTESIAN_POINT ( 'NONE',  ( 21.72449340488910607, 10.28395627750226815, -188.3499999999999659 ) ) ;
#116213=DIRECTION ( 'NONE',  ( -0.000000000000000000, -0.000000000000000000, -1.000000000000000000 ) ) ;
#116253=CARTESIAN_POINT ( 'NONE',  ( -16.93262454970420094, 10.00202046794151300, -180.0729237737626534 ) ) ;
#116420=VERTEX_POINT ( 'NONE', #135128 ) ;
#116492=EDGE_CURVE ( 'NONE', #54060, #57422, #154739, .T. ) ;
#116555=CARTESIAN_POINT ( 'NONE',  ( -16.93521499325732549, 9.994786119814676795, -188.4071085410935211 ) ) ;
#116744=ORIENTED_EDGE ( 'NONE', *, *, #17207, .T. ) ;
#117025=VECTOR ( 'NONE', #117986, 1000.000000000000000 ) ;
#117087=FACE_OUTER_BOUND ( 'NONE', #150458, .T. ) ;
#117333=CARTESIAN_POINT ( 'NONE',  ( -16.81744102076748959, 9.950000000011138823, -188.3499999999999659 ) ) ;
#117511=DIRECTION ( 'NONE',  ( -1.000000000000000000, 0.000000000000000000, 0.000000000000000000 ) ) ;
#117586=ORIENTED_EDGE ( 'NONE', *, *, #233623, .T. ) ;
#117804=ORIENTED_EDGE ( 'NONE', *, *, #29649, .T. ) ;
#117933=VECTOR ( 'NONE', #82797, 1000.000000000000000 ) ;
#117986=DIRECTION ( 'NONE',  ( 1.000000000000000000, 0.000000000000000000, 0.000000000000000000 ) ) ;
#118470=B_SPLINE_CURVE_WITH_KNOTS ( 'NONE', 3,
 ( #105617, #165640, #24860, #226874, #204731, #46935, #28731, #84760, #221716, #146047, #143485, #163080, #23588 ),
 .UNSPECIFIED., .F., .F.,
 ( 4, 3, 3, 3, 4 ),
 ( 1.110764993427085326E-16, 1.946463881814652902E-05, 3.922356109943681788E-05, 4.215060953237600338E-05, 4.415117091092905685E-05 ),
 .UNSPECIFIED. ) ;
#118473=CARTESIAN_POINT ( 'NONE',  ( 18.54999999999999716, 9.950000000011153034, -188.3500000000000227 ) ) ;
#118535=CARTESIAN_POINT ( 'NONE',  ( -16.87036670365548474, 10.08494996326643189, -188.4499999999999886 ) ) ;
#118649=CARTESIAN_POINT ( 'NONE',  ( 15.51872946208854565, 9.376580978055097049, -185.1269462470118867 ) ) ;
#118777=AXIS2_PLACEMENT_3D ( 'NONE', #50865, #109570, #151300 ) ;
#118819=CARTESIAN_POINT ( 'NONE',  ( -16.93583594267724379, 10.00862343506335961, -180.0593908393207414 ) ) ;
#118894=VECTOR ( 'NONE', #35742, 1000.000000000000000 ) ;
#119191=CARTESIAN_POINT ( 'NONE',  ( -14.56556274378147542, 9.446557523083688679, -182.5899419543458464 ) ) ;
#119485=CARTESIAN_POINT ( 'NONE',  ( 20.27550659511088682, 9.216043722520002035, -176.7499999999999716 ) ) ;
#119734=EDGE_LOOP ( 'NONE', ( #108630, #173999, #73142, #53694, #140259 ) ) ;
#119736=CARTESIAN_POINT ( 'NONE',  ( -16.94165728009537375, 9.987869755934932314, -188.3910550085101363 ) ) ;
#119817=CARTESIAN_POINT ( 'NONE',  ( -16.91256925476571027, 9.985731158139333985, -180.0323575109946717 ) ) ;
#119827=DIRECTION ( 'NONE',  ( 1.652117596168391700E-15, 1.000000000000000000, -0.000000000000000000 ) ) ;
#119883=EDGE_LOOP ( 'NONE', ( #139325, #18712, #236792, #187058 ) ) ;
#119936=CARTESIAN_POINT ( 'NONE',  ( -16.77732147262506146, 9.945966932629788815, -188.3364912432758445 ) ) ;
#120198=EDGE_LOOP ( 'NONE', ( #52146, #58464, #29397, #29173, #172378, #226334, #21256, #157128, #202063, #13059 ) ) ;
#120238=CARTESIAN_POINT ( 'NONE',  ( -16.85722902420149083, 9.950000000011076651, -188.2344525262296600 ) ) ;
#120468=CARTESIAN_POINT ( 'NONE',  ( -18.40000000000000213, 11.75000000001113953, -180.1499999999999773 ) ) ;
#120498=CARTESIAN_POINT ( 'NONE',  ( -14.87779219673428521, 9.430633469083948839, -182.7317657948240424 ) ) ;
#120503=CYLINDRICAL_SURFACE ( 'NONE', #86756, 0.9000000000000014655 ) ;
#120604=CARTESIAN_POINT ( 'NONE',  ( 23.24999999999999645, 11.75000000001113953, -176.7499999999999716 ) ) ;
#120681=CYLINDRICAL_SURFACE ( 'NONE', #72124, 1.749999999999999778 ) ;
#120709=LINE ( 'NONE', #138919, #117933 ) ;
#120824=ORIENTED_EDGE ( 'NONE', *, *, #58873, .F. ) ;
#120949=CARTESIAN_POINT ( 'NONE',  ( -16.86337532320261090, 9.979967204235514089, -188.4489244689827956 ) ) ;
#120954=ORIENTED_EDGE ( 'NONE', *, *, #80500, .T. ) ;
#121048=VECTOR ( 'NONE', #116213, 1000.000000000000000 ) ;
#121411=CARTESIAN_POINT ( 'NONE',  ( -16.93710578446423654, 9.950000000011137047, -180.4188039837998474 ) ) ;
#121567=CYLINDRICAL_SURFACE ( 'NONE', #13926, 0.09999999999998898659 ) ;
#121576=CARTESIAN_POINT ( 'NONE',  ( 15.74999999999999645, 9.850000000011137402, -184.2499999999999716 ) ) ;
#121680=ORIENTED_EDGE ( 'NONE', *, *, #20948, .F. ) ;
#121773=CARTESIAN_POINT ( 'NONE',  ( -12.84409460144753901, 9.410682294279109072, -182.9311434419482225 ) ) ;
#121904=LINE ( 'NONE', #97139, #193090 ) ;
#122016=CARTESIAN_POINT ( 'NONE',  ( -16.92507428761701860, 9.950000000011138823, -188.2866025403783965 ) ) ;
#122096=DIRECTION ( 'NONE',  ( 0.000000000000000000, -0.000000000000000000, -1.000000000000000000 ) ) ;
#122318=ORIENTED_EDGE ( 'NONE', *, *, #107112, .T. ) ;
#122509=DIRECTION ( 'NONE',  ( -1.000000000000000000, -0.000000000000000000, 1.073024830501117725E-15 ) ) ;
#122650=EDGE_LOOP ( 'NONE', ( #111816, #219570 ) ) ;
#123042=DIRECTION ( 'NONE',  ( 1.186688945009010077E-16, -1.000000000000000000, -0.000000000000000000 ) ) ;
#123234=ORIENTED_EDGE ( 'NONE', *, *, #63235, .F. ) ;
#123301=CARTESIAN_POINT ( 'NONE',  ( -16.97683809663752186, 9.950000000011138823, -180.9023640181964652 ) ) ;
#123578=DIRECTION ( 'NONE',  ( -0.000000000000000000, -0.000000000000000000, -1.000000000000000000 ) ) ;
#124155=ORIENTED_EDGE ( 'NONE', *, *, #40530, .F. ) ;
#124212=CARTESIAN_POINT ( 'NONE',  ( -16.89268316805466341, 9.951721813253341153, -180.1442475214544174 ) ) ;
#124682=VECTOR ( 'NONE', #19585, 1000.000000000000000 ) ;
#124839=EDGE_CURVE ( 'NONE', #116420, #4251, #163081, .T. ) ;
#124848=DIRECTION ( 'NONE',  ( -0.000000000000000000, 1.000000000000000000, -0.000000000000000000 ) ) ;
#124891=B_SPLINE_CURVE_WITH_KNOTS ( 'NONE', 3,
 ( #236058, #238634, #20898, #182531, #178693, #3870, #239928, #221608, #78257, #22172 ),
 .UNSPECIFIED., .F., .F.,
 ( 4, 3, 3, 4 ),
 ( 0.000000000000000000, 1.004626015991471073E-05, 1.831183478184062558E-05, 2.062343583996205056E-05 ),
 .UNSPECIFIED. ) ;
#124937=CARTESIAN_POINT ( 'NONE',  ( -17.73285935862606877, 10.85798180379781819, -177.7414381902257787 ) ) ;
#125181=CARTESIAN_POINT ( 'NONE',  ( -16.87372397896795562, 9.880599536652889370, -187.8507245100357181 ) ) ;
#125184=DIRECTION ( 'NONE',  ( 1.000000000000000000, 0.000000000000000000, 0.000000000000000000 ) ) ;
#125197=EDGE_CURVE ( 'NONE', #31330, #10681, #75092, .T. ) ;
#125276=CIRCLE ( 'NONE', #75216, 14.20833333333333748 ) ;
#125340=CARTESIAN_POINT ( 'NONE',  ( -16.79270642812294767, 9.946244216949358119, -188.3389332785629335 ) ) ;
#125504=DIRECTION ( 'NONE',  ( -0.000000000000000000, -0.000000000000000000, -1.000000000000000000 ) ) ;
#125591=CARTESIAN_POINT ( 'NONE',  ( -20.65000000000000568, 7.250000000011138646, -176.7499999999999716 ) ) ;
#125986=CARTESIAN_POINT ( 'NONE',  ( -18.40000000000000213, 11.47316190337364183, -188.4499999999999886 ) ) ;
#126126=EDGE_CURVE ( 'NONE', #232305, #107596, #207175, .T. ) ;
#126284=EDGE_CURVE ( 'NONE', #34916, #169346, #194705, .T. ) ;
#126450=B_SPLINE_CURVE_WITH_KNOTS ( 'NONE', 3,
 ( #189277, #37918, #232268, #174893 ),
 .UNSPECIFIED., .F., .F.,
 ( 4, 4 ),
 ( 0.000000000000000000, 7.713889350930393175E-05 ),
 .UNSPECIFIED. ) ;
#126481=CARTESIAN_POINT ( 'NONE',  ( -18.39999999999999858, 11.75000000001113953, -176.7499999999999716 ) ) ;
#126669=AXIS2_PLACEMENT_3D ( 'NONE', #158509, #97172, #196314 ) ;
#126734=DIRECTION ( 'NONE',  ( -1.000000000000000000, 0.000000000000000000, 1.073024830501117725E-15 ) ) ;
#127043=( BOUNDED_CURVE ( )  B_SPLINE_CURVE ( 3, ( #125986, #108986, #146823, #89425 ),
 .UNSPECIFIED., .F., .F. ) 
 B_SPLINE_CURVE_WITH_KNOTS ( ( 4, 4 ),
 ( 0.000000000000000000, 1.570796326794896558 ),
 .UNSPECIFIED. ) 
 CURVE ( )  GEOMETRIC_REPRESENTATION_ITEM ( )  RATIONAL_B_SPLINE_CURVE ( ( 1.000000000000000000, 0.8047378541243649375, 0.8047378541243649375, 1.000000000000000000 ) ) 
 REPRESENTATION_ITEM ( '' )  );
#127684=VECTOR ( 'NONE', #241035, 1000.000000000000000 ) ;
#127858=( BOUNDED_SURFACE ( )  B_SPLINE_SURFACE ( 3, 2, ( 
 ( #164274, #243793, #46857 ),
 ( #248943, #148555, #228095 ),
 ( #65146, #204650, #245077 ),
 ( #147257, #70328, #183818 ) ),
 .UNSPECIFIED., .F., .F., .F. ) 
 B_SPLINE_SURFACE_WITH_KNOTS ( ( 4, 4 ),
 ( 3, 3 ),
 ( 4.712388980384689674, 5.765869716888459173 ),
 ( 0.000000000000000000, 1.000000000000000000 ),
 .UNSPECIFIED. ) 
 GEOMETRIC_REPRESENTATION_ITEM ( )  RATIONAL_B_SPLINE_SURFACE ( (
 ( 1.000000000000000000, 0.7071067811864494290, 1.000000000000000000),
 ( 1.000000000000000000, 0.7953136715914208565, 1.000000000000000000),
 ( 1.000000000000000000, 0.8646876308614606099, 1.000000000000000000),
 ( 1.000000000000000000, 0.8984936768950610997, 1.000000000000000000) ) ) 
 REPRESENTATION_ITEM ( '' )  SURFACE ( )  );
#127911=CARTESIAN_POINT ( 'NONE',  ( -16.88783316861808714, 9.950000000011137047, -188.2477359580206837 ) ) ;
#128104=VECTOR ( 'NONE', #88672, 1000.000000000000000 ) ;
#128136=EDGE_CURVE ( 'NONE', #6394, #54060, #141814, .T. ) ;
#128343=EDGE_LOOP ( 'NONE', ( #101963, #37369, #65957, #188781 ) ) ;
#128384=ORIENTED_EDGE ( 'NONE', *, *, #209514, .T. ) ;
#128458=PRODUCT_DEFINITION_SHAPE ( 'NONE', 'NONE',  #62861 ) ;
#128754=LINE ( 'NONE', #68774, #3398 ) ;
#128877=EDGE_CURVE ( 'NONE', #67768, #218279, #81232, .T. ) ;
#129032=CARTESIAN_POINT ( 'NONE',  ( -16.80100914604133777, 9.943149094114717812, -188.3170441272875451 ) ) ;
#129080=CARTESIAN_POINT ( 'NONE',  ( -16.80621392010912984, 9.942202577518864715, -180.1895919654171507 ) ) ;
#129103=AXIS2_PLACEMENT_3D ( 'NONE', #42502, #37400, #140310 ) ;
#129693=VERTEX_POINT ( 'NONE', #123301 ) ;
#129877=CARTESIAN_POINT ( 'NONE',  ( -16.94445028196807002, 9.992063609708893068, -188.3926698215815350 ) ) ;
#130293=DIRECTION ( 'NONE',  ( -0.000000000000000000, 1.000000000000000000, -0.000000000000000000 ) ) ;
#130459=CIRCLE ( 'NONE', #34814, 0.5000000000000004441 ) ;
#130574=PLANE ( 'NONE',  #77812 ) ;
#130590=DIRECTION ( 'NONE',  ( 0.000000000000000000, 0.000000000000000000, 1.000000000000000000 ) ) ;
#130811=CYLINDRICAL_SURFACE ( 'NONE', #54448, 0.1000000000000001443 ) ;
#131101=AXIS2_PLACEMENT_3D ( 'NONE', #81787, #161381, #221315 ) ;
#131333=CARTESIAN_POINT ( 'NONE',  ( -12.25000000000000178, 9.350000000011139178, -184.2499999999999716 ) ) ;
#131422=VERTEX_POINT ( 'NONE', #254507 ) ;
#131437=B_SPLINE_CURVE_WITH_KNOTS ( 'NONE', 3,
 ( #89830, #87258, #108131, #186398, #187687, #188951, #7753, #9028, #110692, #70318 ),
 .UNSPECIFIED., .F., .F.,
 ( 4, 3, 3, 4 ),
 ( 1.886399917053072492E-15, 3.877043166999333273E-05, 7.336897548476527698E-05, 7.659383120239750958E-05 ),
 .UNSPECIFIED. ) ;
#131439=( GEOMETRIC_REPRESENTATION_CONTEXT ( 3 ) GLOBAL_UNCERTAINTY_ASSIGNED_CONTEXT ( ( #50349 ) ) GLOBAL_UNIT_ASSIGNED_CONTEXT ( ( #161166, #159896, #101126 ) ) REPRESENTATION_CONTEXT ( 'NONE', 'WORKASPACE' ) );
#131534=ORIENTED_EDGE ( 'NONE', *, *, #216857, .F. ) ;
#131636=CARTESIAN_POINT ( 'NONE',  ( -16.84793658983456410, 9.950000000011197443, -180.2336466778095314 ) ) ;
#131670=CARTESIAN_POINT ( 'NONE',  ( -17.11825945287482753, 10.05000000001113847, -180.2499999999999716 ) ) ;
#131692=EDGE_LOOP ( 'NONE', ( #150959, #238553, #195552, #138686 ) ) ;
#131768=DIRECTION ( 'NONE',  ( 1.000000000000000000, 0.000000000000000000, -1.020425574104004196E-15 ) ) ;
#131792=EDGE_CURVE ( 'NONE', #179647, #114189, #35367, .T. ) ;
#132098=CARTESIAN_POINT ( 'NONE',  ( -18.34374000495059676, 11.47316190337362940, -191.7499999999999716 ) ) ;
#132159=VECTOR ( 'NONE', #119827, 1000.000000000000000 ) ;
#132214=ORIENTED_EDGE ( 'NONE', *, *, #5849, .T. ) ;
#132427=CARTESIAN_POINT ( 'NONE',  ( 12.33938619321248176, 9.360723793997193454, -184.8139271946066913 ) ) ;
#132433=CYLINDRICAL_SURFACE ( 'NONE', #175908, 1.500000000000001332 ) ;
#132485=CARTESIAN_POINT ( 'NONE',  ( -18.40000000000000213, 11.48667500176882328, -176.7499999999999716 ) ) ;
#132628=CARTESIAN_POINT ( 'NONE',  ( -12.48127053791144903, 9.376580978055093496, -185.1269462470118867 ) ) ;
#132701=ORIENTED_EDGE ( 'NONE', *, *, #137107, .T. ) ;
#132753=( GEOMETRIC_REPRESENTATION_CONTEXT ( 3 ) GLOBAL_UNCERTAINTY_ASSIGNED_CONTEXT ( ( #86912 ) ) GLOBAL_UNIT_ASSIGNED_CONTEXT ( ( #166978, #65264, #186512 ) ) REPRESENTATION_CONTEXT ( 'NONE', 'WORKASPACE' ) );
#133014=ORIENTED_EDGE ( 'NONE', *, *, #163862, .T. ) ;
#133842=ADVANCED_FACE ( 'NONE', ( #206299 ), #120681, .F. ) ;
#134027=DIRECTION ( 'NONE',  ( 1.000000000000000000, 0.000000000000000000, 0.000000000000000000 ) ) ;
#134167=ADVANCED_FACE ( 'NONE', ( #96588 ), #255643, .F. ) ;
#134738=VERTEX_POINT ( 'NONE', #21916 ) ;
#134804=CARTESIAN_POINT ( 'NONE',  ( -16.93294127766158752, 10.00328010296601988, -188.4299072658292005 ) ) ;
#134979=ORIENTED_EDGE ( 'NONE', *, *, #226229, .T. ) ;
#135128=CARTESIAN_POINT ( 'NONE',  ( -21.64999999999999858, 10.05000000001113847, -180.1499999999999773 ) ) ;
#135156=VECTOR ( 'NONE', #179197, 1000.000000000000000 ) ;
#135160=DIRECTION ( 'NONE',  ( 0.000000000000000000, 0.000000000000000000, 1.000000000000000000 ) ) ;
#135207=ORIENTED_EDGE ( 'NONE', *, *, #155753, .T. ) ;
#135418=FACE_OUTER_BOUND ( 'NONE', #52091, .T. ) ;
#135515=CARTESIAN_POINT ( 'NONE',  ( -18.40000000000000213, 5.650000000011139001, -188.3499999999999659 ) ) ;
#135518=( GEOMETRIC_REPRESENTATION_CONTEXT ( 3 ) GLOBAL_UNCERTAINTY_ASSIGNED_CONTEXT ( ( #253699 ) ) GLOBAL_UNIT_ASSIGNED_CONTEXT ( ( #80301, #60758, #187164 ) ) REPRESENTATION_CONTEXT ( 'NONE', 'WORKASPACE' ) );
#135556=CARTESIAN_POINT ( 'NONE',  ( -16.81744102076748959, 9.950000000011138823, -188.3499999999999659 ) ) ;
#135684=CARTESIAN_POINT ( 'NONE',  ( -16.90202395485531639, 9.965944544560510820, -188.4030137212579916 ) ) ;
#135782=CARTESIAN_POINT ( 'NONE',  ( -16.93440969289731157, 9.995185175825108459, -180.0912341850107623 ) ) ;
#135840=CARTESIAN_POINT ( 'NONE',  ( -16.88219499860498374, 9.950206425438745228, -180.1493096901072875 ) ) ;
#135873=EDGE_CURVE ( 'NONE', #111909, #211794, #121904, .T. ) ;
#136064=AXIS2_PLACEMENT_3D ( 'NONE', #213311, #34711, #51651 ) ;
#136128=VECTOR ( 'NONE', #200123, 1000.000000000000000 ) ;
#136198=CARTESIAN_POINT ( 'NONE',  ( 23.04999999999999716, 8.822561741677553471, -188.3499999999999659 ) ) ;
#136202=VECTOR ( 'NONE', #254621, 1000.000000000000000 ) ;
#136282=ORIENTED_EDGE ( 'NONE', *, *, #248831, .F. ) ;
#136433=ORIENTED_EDGE ( 'NONE', *, *, #235329, .T. ) ;
#136526=FACE_OUTER_BOUND ( 'NONE', #204378, .T. ) ;
#136660=VERTEX_POINT ( 'NONE', #107775 ) ;
#136848=CARTESIAN_POINT ( 'NONE',  ( -16.97048361161167662, 9.950000000011137047, -187.8588843444303507 ) ) ;
#137011=STYLED_ITEM ( 'NONE', ( #44436 ), #191235 ) ;
#137082=CARTESIAN_POINT ( 'NONE',  ( -16.93302609847409457, 9.996682520814371031, -180.0863884953625131 ) ) ;
#137107=EDGE_CURVE ( 'NONE', #255276, #190492, #126450, .T. ) ;
#137383=EDGE_LOOP ( 'NONE', ( #108144, #152219, #208632 ) ) ;
#137402=ADVANCED_FACE ( 'NONE', ( #207255 ), #127858, .T. ) ;
#137665=ORIENTED_EDGE ( 'NONE', *, *, #63203, .T. ) ;
#137678=EDGE_LOOP ( 'NONE', ( #209034, #109968, #229514, #242802 ) ) ;
#137809=B_SPLINE_CURVE_WITH_KNOTS ( 'NONE', 3,
 ( #19337, #180988, #98831, #62314, #119736, #141839, #239673, #41487, #248646, #146963, #148264, #85683, #68735 ),
 .UNSPECIFIED., .F., .F.,
 ( 4, 3, 3, 3, 4 ),
 ( -3.224855718284247652E-06, 4.235164736271501695E-22, 6.199515528661409170E-06, 4.034952380126323066E-05, 7.452715123697944196E-05 ),
 .UNSPECIFIED. ) ;
#137892=CARTESIAN_POINT ( 'NONE',  ( -16.86379686415369150, 9.975217759264314310, -188.4333898890902503 ) ) ;
#137907=DIRECTION ( 'NONE',  ( -0.5932847527679298016, 0.8049926720990051576, 0.000000000000000000 ) ) ;
#137977=CARTESIAN_POINT ( 'NONE',  ( -16.94878442675512531, 9.991729103002162660, -180.1117804243620810 ) ) ;
#138223=DIRECTION ( 'NONE',  ( 1.000000000000000000, -0.000000000000000000, -0.000000000000000000 ) ) ;
#138258=ADVANCED_FACE ( 'NONE', ( #153105 ), #72251, .F. ) ;
#138569=CARTESIAN_POINT ( 'NONE',  ( -16.87331047859651179, 9.950000000011142376, -180.1499999999999773 ) ) ;
#138686=ORIENTED_EDGE ( 'NONE', *, *, #107112, .F. ) ;
#138702=CARTESIAN_POINT ( 'NONE',  ( -15.15766958671843589, 9.410538608540024441, -182.9326879971408175 ) ) ;
#138919=CARTESIAN_POINT ( 'NONE',  ( -23.25000000000000355, 11.75000000001113953, -176.7499999999999716 ) ) ;
#139183=LINE ( 'NONE', #77938, #224374 ) ;
#139325=ORIENTED_EDGE ( 'NONE', *, *, #192639, .F. ) ;
#139373=DIRECTION ( 'NONE',  ( 1.000000000000000000, -0.000000000000000000, -0.000000000000000000 ) ) ;
#139485=CARTESIAN_POINT ( 'NONE',  ( 21.72449340488910252, 10.28395627750227703, -180.1499999999999773 ) ) ;
#139536=CARTESIAN_POINT ( 'NONE',  ( -16.89318236219977365, 9.951535257886286345, -188.3551296321058146 ) ) ;
#139623=CARTESIAN_POINT ( 'NONE',  ( -16.93226657140833069, 9.999543822735571297, -180.0787131109735810 ) ) ;
#139726=CARTESIAN_POINT ( 'NONE',  ( -18.40000000000000213, 11.75000000001113953, -180.1499999999999773 ) ) ;
#139863=CARTESIAN_POINT ( 'NONE',  ( -17.04295772865475556, 10.02489942527111744, -188.3499999999999659 ) ) ;
#139904=ORIENTED_EDGE ( 'NONE', *, *, #113216, .T. ) ;
#140005=CARTESIAN_POINT ( 'NONE',  ( -13.77178122865954002, 9.456028260519072859, -182.5111980350657177 ) ) ;
#140154=AXIS2_PLACEMENT_3D ( 'NONE', #184471, #70988, #67106 ) ;
#140259=ORIENTED_EDGE ( 'NONE', *, *, #209514, .F. ) ;
#140298=FACE_OUTER_BOUND ( 'NONE', #58826, .T. ) ;
#140310=DIRECTION ( 'NONE',  ( -1.186688945009010077E-16, 1.000000000000000000, 0.000000000000000000 ) ) ;
#140384=ORIENTED_EDGE ( 'NONE', *, *, #990, .T. ) ;
#140467=CARTESIAN_POINT ( 'NONE',  ( -16.86733706339143168, 9.965990529650822438, -188.4031153019986675 ) ) ;
#140525=DIRECTION ( 'NONE',  ( 0.000000000000000000, 1.000000000000000000, 0.000000000000000000 ) ) ;
#140752=CARTESIAN_POINT ( 'NONE',  ( 15.57250062127603130, 9.370689921613767126, -185.0264651266610372 ) ) ;
#140947=CARTESIAN_POINT ( 'NONE',  ( -16.96982749440708460, 9.950000000011137047, -180.6247784088108688 ) ) ;
#141005=EDGE_CURVE ( 'NONE', #56652, #232238, #163339, .T. ) ;
#141083=AXIS2_PLACEMENT_3D ( 'NONE', #225527, #152134, #125184 ) ;
#141508=CARTESIAN_POINT ( 'NONE',  ( 15.15590539855245922, 9.410682294279107296, -182.9311434419481941 ) ) ;
#141666=VERTEX_POINT ( 'NONE', #118473 ) ;
#141749=CARTESIAN_POINT ( 'NONE',  ( -17.73285935862007534, 10.85798180380174394, -190.7585618097804456 ) ) ;
#141814=LINE ( 'NONE', #21883, #15799 ) ;
#141839=CARTESIAN_POINT ( 'NONE',  ( -16.94052228080551359, 9.986279733109993728, -188.3903755026694000 ) ) ;
#142211=CARTESIAN_POINT ( 'NONE',  ( -16.87683809663750978, 9.950000000011137047, -180.9023640181964652 ) ) ;
#142469=DIRECTION ( 'NONE',  ( -0.5932847527679310229, 0.8049926720990042694, -6.366092712777067056E-16 ) ) ;
#142499=DIRECTION ( 'NONE',  ( 1.020425574104004196E-15, 1.210927747993693964E-31, 1.000000000000000000 ) ) ;
#142697=ORIENTED_EDGE ( 'NONE', *, *, #216857, .T. ) ;
#142903=AXIS2_PLACEMENT_3D ( 'NONE', #89903, #32550, #72958 ) ;
#142906=FACE_OUTER_BOUND ( 'NONE', #120198, .T. ) ;
#143017=CARTESIAN_POINT ( 'NONE',  ( -17.78241384947038028, 10.85557575281234044, -190.7509623274730188 ) ) ;
#143072=ORIENTED_EDGE ( 'NONE', *, *, #58873, .T. ) ;
#143110=CARTESIAN_POINT ( 'NONE',  ( 18.39999999999999503, 11.47316190337363828, -180.1499999999999773 ) ) ;
#143121=ORIENTED_EDGE ( 'NONE', *, *, #53452, .F. ) ;
#143485=CARTESIAN_POINT ( 'NONE',  ( -16.77779411503078322, 9.946101446935278645, -180.1630574176197968 ) ) ;
#143523=CARTESIAN_POINT ( 'NONE',  ( 13.99999999999999822, 9.850000000011137402, -184.2499999999999716 ) ) ;
#143576=CARTESIAN_POINT ( 'NONE',  ( 20.05000000000002913, 7.250000000011171508, -180.1499999999999773 ) ) ;
#143620=VECTOR ( 'NONE', #113252, 1000.000000000000000 ) ;
#143751=CARTESIAN_POINT ( 'NONE',  ( -16.86757978335471364, 9.965650379045438712, -180.0980046531674930 ) ) ;
#143935=EDGE_CURVE ( 'NONE', #151091, #158360, #128754, .T. ) ;
#143982=LINE ( 'NONE', #120604, #136128 ) ;
#144060=CARTESIAN_POINT ( 'NONE',  ( 15.74999999999999645, 9.350000000011139178, -184.2499999999999716 ) ) ;
#144122=CARTESIAN_POINT ( 'NONE',  ( -17.11825945287481332, 9.950000000011138823, -188.2499999999999716 ) ) ;
#144295=CARTESIAN_POINT ( 'NONE',  ( -16.87036670365547764, 9.989418819312797737, -188.4795601173019861 ) ) ;
#144447=EDGE_CURVE ( 'NONE', #12552, #136660, #250931, .T. ) ;
#144581=LINE ( 'NONE', #85876, #226226 ) ;
#144586=CARTESIAN_POINT ( 'NONE',  ( 12.68104795156994946, 9.396533993965075382, -185.4059397791732806 ) ) ;
#144714=CARTESIAN_POINT ( 'NONE',  ( -18.37160782347004329, 11.47561641481354044, -176.7499999999999716 ) ) ;
#145004=ORIENTED_EDGE ( 'NONE', *, *, #86065, .F. ) ;
#145448=CARTESIAN_POINT ( 'NONE',  ( -23.25000000000000355, 5.650000000011139001, -180.1499999999999773 ) ) ;
#145821=CARTESIAN_POINT ( 'NONE',  ( -16.94445028196807002, 9.992063609708893068, -188.3926698215815350 ) ) ;
#146047=CARTESIAN_POINT ( 'NONE',  ( -16.77828822508139694, 9.946229374931901290, -180.1626282513739170 ) ) ;
#146071=LINE ( 'NONE', #41873, #69247 ) ;
#146114=VERTEX_POINT ( 'NONE', #159319 ) ;
#146411=CARTESIAN_POINT ( 'NONE',  ( -16.83199030136657370, 9.930648033124622742, -180.2724010226574194 ) ) ;
#146480=DIRECTION ( 'NONE',  ( -1.000000000000000000, 0.000000000000000000, 0.000000000000000000 ) ) ;
#146823=CARTESIAN_POINT ( 'NONE',  ( -18.40000000000000213, 11.41458325961095177, -188.3499999999999943 ) ) ;
#146963=CARTESIAN_POINT ( 'NONE',  ( -16.91776028072577631, 9.963400393640901243, -188.3750240147020918 ) ) ;
#147186=DIRECTION ( 'NONE',  ( 0.000000000000000000, 0.000000000000000000, -1.000000000000000000 ) ) ;
#147257=CARTESIAN_POINT ( 'NONE',  ( -16.87242674293850797, 9.950000000011138823, -180.1489097536276063 ) ) ;
#147374=VECTOR ( 'NONE', #208610, 1000.000000000000000 ) ;
#147410=CARTESIAN_POINT ( 'NONE',  ( 13.99999999999999822, 9.850000000011137402, -184.2499999999999716 ) ) ;
#147569=ORIENTED_EDGE ( 'NONE', *, *, #187437, .T. ) ;
#147698=AXIS2_PLACEMENT_3D ( 'NONE', #102951, #7735, #181248 ) ;
#147718=ORIENTED_EDGE ( 'NONE', *, *, #47642, .F. ) ;
#147753=AXIS2_PLACEMENT_3D ( 'NONE', #67491, #247407, #169199 ) ;
#147762=DIRECTION ( 'NONE',  ( 0.000000000000000000, -1.000000000000000000, 0.000000000000000000 ) ) ;
#147902=CARTESIAN_POINT ( 'NONE',  ( -16.95709691156997323, 9.950000000011497647, -188.3399424374871103 ) ) ;
#148253=ADVANCED_FACE ( 'NONE', ( #207924 ), #29304, .F. ) ;
#148264=CARTESIAN_POINT ( 'NONE',  ( -16.90987985657661952, 9.957807518190888274, -188.3692870888836239 ) ) ;
#148302=CARTESIAN_POINT ( 'NONE',  ( -12.25000000000000178, 9.350000000011139178, -184.2499999999999716 ) ) ;
#148423=CARTESIAN_POINT ( 'NONE',  ( 21.72449340488909897, 10.28395627750227703, -188.3499999999999659 ) ) ;
#148555=CARTESIAN_POINT ( 'NONE',  ( -17.05016517655662156, 9.950000000014890489, -180.1726979959937580 ) ) ;
#148598=CARTESIAN_POINT ( 'NONE',  ( -16.83794479845801817, 9.926357419362650703, -188.1964447042223014 ) ) ;
#149329=CIRCLE ( 'NONE', #65918, 0.09999999999998898659 ) ;
#149375=EDGE_LOOP ( 'NONE', ( #37514, #104312, #70221, #81313 ) ) ;
#149439=CARTESIAN_POINT ( 'NONE',  ( 12.84435279558020859, 9.410708747058238899, -185.5692084058441083 ) ) ;
#149440=CIRCLE ( 'NONE', #87025, 0.09999999999999939493 ) ;
#150230=VECTOR ( 'NONE', #184954, 1000.000000000000000 ) ;
#150458=EDGE_LOOP ( 'NONE', ( #177122, #254627, #184518, #170395 ) ) ;
#150584=CIRCLE ( 'NONE', #171464, 14.30833333333333890 ) ;
#150735=CARTESIAN_POINT ( 'NONE',  ( -18.40000000000000213, 11.75000000001113953, -191.7499999999999716 ) ) ;
#150902=CARTESIAN_POINT ( 'NONE',  ( -15.69373346032659455, 9.356790025057037496, -184.7048265086138770 ) ) ;
#150959=ORIENTED_EDGE ( 'NONE', *, *, #232251, .F. ) ;
#151091=VERTEX_POINT ( 'NONE', #27588 ) ;
#151122=AXIS2_PLACEMENT_3D ( 'NONE', #8098, #87600, #130590 ) ;
#151166=CARTESIAN_POINT ( 'NONE',  ( -18.40000000000000213, 5.650000000011139001, -188.3499999999999659 ) ) ;
#151221=VERTEX_POINT ( 'NONE', #95220 ) ;
#151300=DIRECTION ( 'NONE',  ( -1.020425574104004196E-15, -1.210927747993693964E-31, 1.000000000000000000 ) ) ;
#151399=CARTESIAN_POINT ( 'NONE',  ( 20.05000000000002913, 7.250000000011171508, -188.3499999999999659 ) ) ;
#151480=AXIS2_PLACEMENT_3D ( 'NONE', #154385, #51352, #110073 ) ;
#151596=ORIENTED_EDGE ( 'NONE', *, *, #222296, .T. ) ;
#151957=CARTESIAN_POINT ( 'NONE',  ( -18.40000000000000213, 11.75000000001113953, -191.7499999999999716 ) ) ;
#152134=DIRECTION ( 'NONE',  ( 1.073024830501117725E-15, -0.000000000000000000, -1.000000000000000000 ) ) ;
#152219=ORIENTED_EDGE ( 'NONE', *, *, #55800, .T. ) ;
#152323=ORIENTED_EDGE ( 'NONE', *, *, #116492, .F. ) ;
#152372=ORIENTED_EDGE ( 'NONE', *, *, #83020, .F. ) ;
#152568=CARTESIAN_POINT ( 'NONE',  ( 20.73486653747088582, 7.250000000011182166, -188.3499999999999659 ) ) ;
#152639=LINE ( 'NONE', #110908, #63214 ) ;
#153105=FACE_OUTER_BOUND ( 'NONE', #11064, .T. ) ;
#153513=CARTESIAN_POINT ( 'NONE',  ( 0.000000000000000000, 0.000000000000000000, 0.000000000000000000 ) ) ;
#153583=DIRECTION ( 'NONE',  ( -1.000000000000000000, 0.000000000000000000, 0.000000000000000000 ) ) ;
#153605=CIRCLE ( 'NONE', #141083, 0.9000000000000014655 ) ;
#154156=AXIS2_PLACEMENT_3D ( 'NONE', #179230, #230529, #12779 ) ;
#154190=LINE ( 'NONE', #255766, #216436 ) ;
#154207=CARTESIAN_POINT ( 'NONE',  ( -18.40000000000000213, 11.47316190337362762, -180.0499999999999545 ) ) ;
#154353=AXIS2_PLACEMENT_3D ( 'NONE', #246250, #204542, #225377 ) ;
#154385=CARTESIAN_POINT ( 'NONE',  ( 18.54999999999999716, 8.750000000011182166, -176.7499999999999716 ) ) ;
#154432=ORIENTED_EDGE ( 'NONE', *, *, #6884, .F. ) ;
#154434=CARTESIAN_POINT ( 'NONE',  ( -16.93262454970419384, 10.00202046794151478, -188.4270762262372898 ) ) ;
#154560=( BOUNDED_SURFACE ( )  B_SPLINE_SURFACE ( 3, 2, ( 
 ( #158871, #218803, #256602 ),
 ( #55863, #96284, #177158 ),
 ( #40211, #97554, #238375 ),
 ( #137977, #36359, #100124 ) ),
 .UNSPECIFIED., .F., .F., .F. ) 
 B_SPLINE_SURFACE_WITH_KNOTS ( ( 4, 4 ),
 ( 3, 3 ),
 ( 0.0008258556059633777964, 0.0009616864997632713560 ),
 ( 0.000000000000000000, 1.000000000000000000 ),
 .UNSPECIFIED. ) 
 GEOMETRIC_REPRESENTATION_ITEM ( )  RATIONAL_B_SPLINE_SURFACE ( (
 ( 1.000000000000000000, 0.9152888060719425178, 1.000000000000000000),
 ( 1.000000000000000000, 0.9327727094138110742, 1.000000000000000000),
 ( 1.000000000000000000, 0.9369023509258611604, 1.000000000000000000),
 ( 1.000000000000000000, 0.9246339933864502481, 1.000000000000000000) ) ) 
 REPRESENTATION_ITEM ( '' )  SURFACE ( )  );
#154565=CARTESIAN_POINT ( 'NONE',  ( 23.04999999999999716, 8.822561741677553471, -180.1499999999999773 ) ) ;
#154572=VERTEX_POINT ( 'NONE', #222448 ) ;
#154639=LINE ( 'NONE', #254927, #58702 ) ;
#154739=LINE ( 'NONE', #200259, #30696 ) ;
#155023=VECTOR ( 'NONE', #112337, 1000.000000000000000 ) ;
#155108=ORIENTED_EDGE ( 'NONE', *, *, #219278, .T. ) ;
#155353=ORIENTED_EDGE ( 'NONE', *, *, #20925, .F. ) ;
#155400=FACE_OUTER_BOUND ( 'NONE', #47456, .T. ) ;
#155463=EDGE_CURVE ( 'NONE', #181967, #51363, #152639, .T. ) ;
#155468=CARTESIAN_POINT ( 'NONE',  ( -16.87383368123029825, 9.950000000011138823, -180.1499999999999773 ) ) ;
#155469=DIRECTION ( 'NONE',  ( -0.000000000000000000, -0.000000000000000000, 1.000000000000000000 ) ) ;
#155632=CARTESIAN_POINT ( 'NONE',  ( -17.11825945287481687, 9.950000000011138823, -188.2499999999999716 ) ) ;
#155753=EDGE_CURVE ( 'NONE', #151091, #146114, #87170, .T. ) ;
#156226=EDGE_CURVE ( 'NONE', #13123, #111385, #78537, .T. ) ;
#156460=CARTESIAN_POINT ( 'NONE',  ( -16.97683809663754673, 9.950000000011137047, -187.7284708321105029 ) ) ;
#156510=ORIENTED_EDGE ( 'NONE', *, *, #237508, .T. ) ;
#156911=LINE ( 'NONE', #214291, #54286 ) ;
#156996=VERTEX_POINT ( 'NONE', #74118 ) ;
#157112=VECTOR ( 'NONE', #20724, 1000.000000000000000 ) ;
#157128=ORIENTED_EDGE ( 'NONE', *, *, #131792, .T. ) ;
#157600=CYLINDRICAL_SURFACE ( 'NONE', #248901, 0.1999999999999987899 ) ;
#158001=ORIENTED_EDGE ( 'NONE', *, *, #1875, .T. ) ;
#158075=ADVANCED_FACE ( 'NONE', ( #215103 ), #249116, .F. ) ;
#158091=CARTESIAN_POINT ( 'NONE',  ( -16.88705144915408596, 9.950000000011078427, -188.0690214052869749 ) ) ;
#158136=CARTESIAN_POINT ( 'NONE',  ( 20.73486653747090003, 7.250000000011182166, -188.3499999999999659 ) ) ;
#158151=ORIENTED_EDGE ( 'NONE', *, *, #7855, .F. ) ;
#158360=VERTEX_POINT ( 'NONE', #126481 ) ;
#158509=CARTESIAN_POINT ( 'NONE',  ( -23.25000000000000355, 10.05000000001113847, -188.2499999999999716 ) ) ;
#158620=PRESENTATION_STYLE_ASSIGNMENT (( #241975 ) ) ;
#158730=CARTESIAN_POINT ( 'NONE',  ( -21.65000000000000213, 7.250000000011138646, -176.7499999999999716 ) ) ;
#158762=CARTESIAN_POINT ( 'NONE',  ( 18.39999999999999503, 11.75000000001113953, -191.7499999999999716 ) ) ;
#158871=CARTESIAN_POINT ( 'NONE',  ( -16.94107738177415712, 10.01423928514777550, -180.0499999999999545 ) ) ;
#158876=ORIENTED_EDGE ( 'NONE', *, *, #7855, .T. ) ;
#159010=EDGE_LOOP ( 'NONE', ( #135207, #73291, #156510, #117804 ) ) ;
#159263=DIRECTION ( 'NONE',  ( 1.186688945009010077E-16, -1.000000000000000000, -0.000000000000000000 ) ) ;
#159319=CARTESIAN_POINT ( 'NONE',  ( 18.39999999999998082, 11.47316190337362585, -176.7499999999999716 ) ) ;
#159345=CARTESIAN_POINT ( 'NONE',  ( -16.92280123533721792, 9.950000000011137047, -188.1493676859139157 ) ) ;
#159349=CARTESIAN_POINT ( 'NONE',  ( -20.65000000000000568, 7.250000000011138646, -176.7499999999999716 ) ) ;
#159445=CARTESIAN_POINT ( 'NONE',  ( -17.78043020864320667, 10.85359211201683927, -177.8369508342797474 ) ) ;
#159483=CARTESIAN_POINT ( 'NONE',  ( -23.25000000000000355, 11.75000000001113953, -188.3499999999999659 ) ) ;
#159680=EDGE_CURVE ( 'NONE', #2708, #156996, #80652, .T. ) ;
#159690=EDGE_CURVE ( 'NONE', #151221, #58482, #199357, .T. ) ;
#159809=CARTESIAN_POINT ( 'NONE',  ( 15.06592377766031809, 9.417789466963361278, -182.8573845439768206 ) ) ;
#159896=( NAMED_UNIT ( * ) PLANE_ANGLE_UNIT ( ) SI_UNIT ( $, .RADIAN. ) );
#160069=CARTESIAN_POINT ( 'NONE',  ( -16.86420534634261514, 9.970615445602874161, -188.4183365492373525 ) ) ;
#160396=CARTESIAN_POINT ( 'NONE',  ( -18.40000000000000213, 5.650000000011139001, -191.7499999999999716 ) ) ;
#160889=ORIENTED_EDGE ( 'NONE', *, *, #168921, .T. ) ;
#161166=( LENGTH_UNIT ( ) NAMED_UNIT ( * ) SI_UNIT ( .MILLI., .METRE. ) );
#161381=DIRECTION ( 'NONE',  ( 1.000000000000000000, 0.000000000000000000, 0.000000000000000000 ) ) ;
#161752=CARTESIAN_POINT ( 'NONE',  ( -18.34804628011471195, 11.47316190337353525, -176.7499999999999716 ) ) ;
#161798=LINE ( 'NONE', #199640, #50723 ) ;
#162185=CARTESIAN_POINT ( 'NONE',  ( -12.25000000000000355, 9.350000000011133849, -184.0185689574025787 ) ) ;
#162459=FILL_AREA_STYLE ('',( #219840 ) ) ;
#162574=DIRECTION ( 'NONE',  ( -0.000000000000000000, -0.000000000000000000, -1.000000000000000000 ) ) ;
#162726=EDGE_CURVE ( 'NONE', #13877, #189000, #181235, .T. ) ;
#163073=CARTESIAN_POINT ( 'NONE',  ( 18.39999999999999503, 11.75000000001113953, -191.7499999999999716 ) ) ;
#163080=CARTESIAN_POINT ( 'NONE',  ( -16.77732147278574715, 9.945966932584589415, -180.1635087568757854 ) ) ;
#163081=LINE ( 'NONE', #242580, #218883 ) ;
#163209=ORIENTED_EDGE ( 'NONE', *, *, #990, .F. ) ;
#163255=DIRECTION ( 'NONE',  ( 0.000000000000000000, -1.000000000000000000, 0.000000000000000000 ) ) ;
#163284=ORIENTED_EDGE ( 'NONE', *, *, #183640, .T. ) ;
#163339=LINE ( 'NONE', #164622, #23015 ) ;
#163348=CARTESIAN_POINT ( 'NONE',  ( 17.74533788810830259, 10.81849979148194940, -177.8136226749475384 ) ) ;
#163440=DIRECTION ( 'NONE',  ( -3.035766082959430717E-14, 0.000000000000000000, -1.000000000000000000 ) ) ;
#163605=ORIENTED_EDGE ( 'NONE', *, *, #182684, .F. ) ;
#163673=ORIENTED_EDGE ( 'NONE', *, *, #236961, .T. ) ;
#163755=ORIENTED_EDGE ( 'NONE', *, *, #216639, .T. ) ;
#163839=DIRECTION ( 'NONE',  ( 1.000000000000000000, 0.000000000000000000, 0.000000000000000000 ) ) ;
#163862=EDGE_CURVE ( 'NONE', #107596, #77200, #156911, .T. ) ;
#164098=EDGE_CURVE ( 'NONE', #146114, #71159, #54575, .T. ) ;
#164221=EDGE_LOOP ( 'NONE', ( #21820, #207813, #193031, #250521 ) ) ;
#164274=CARTESIAN_POINT ( 'NONE',  ( -17.11825945287482753, 9.950000000011138823, -180.2499999999999716 ) ) ;
#164309=CARTESIAN_POINT ( 'NONE',  ( -18.34374000495060386, 11.47316190337362585, -176.7499999999999716 ) ) ;
#164429=CARTESIAN_POINT ( 'NONE',  ( 18.54999999999999716, 23.65833333334447985, -184.2499999999999716 ) ) ;
#164622=CARTESIAN_POINT ( 'NONE',  ( 20.27550659511089037, 9.216043722519994930, -188.3499999999999659 ) ) ;
#164819=CARTESIAN_POINT ( 'NONE',  ( 18.39999999999997371, 11.47316190337362940, -191.7499999999999716 ) ) ;
#164928=CARTESIAN_POINT ( 'NONE',  ( 15.70340296795548163, 9.355888454513701546, -183.7886428967779864 ) ) ;
#165089=ORIENTED_EDGE ( 'NONE', *, *, #80500, .F. ) ;
#165119=CARTESIAN_POINT ( 'NONE',  ( -14.00000000000000178, 9.850000000011133849, -184.2499999999999716 ) ) ;
#165640=CARTESIAN_POINT ( 'NONE',  ( -16.81095280782810875, 9.950000000011138823, -180.1499999999990962 ) ) ;
#165851=ORIENTED_EDGE ( 'NONE', *, *, #159680, .F. ) ;
#165903=ORIENTED_EDGE ( 'NONE', *, *, #33345, .T. ) ;
#165955=VERTEX_POINT ( 'NONE', #95704 ) ;
#166003=CARTESIAN_POINT ( 'NONE',  ( 15.48841904831874849, 8.561580951692381092, -180.1499999999999773 ) ) ;
#166065=B_SPLINE_CURVE_WITH_KNOTS ( 'NONE', 3,
 ( #254729, #39620, #197363, #196094, #16192, #134804, #154434, #436, #214366, #35757, #79956, #116555, #115267, #17446, #232668, #54006 ),
 .UNSPECIFIED., .F., .F.,
 ( 4, 3, 3, 3, 3, 4 ),
 ( 0.000000000000000000, 1.810570668010836920E-05, 2.740575833572790496E-05, 4.256816319437009604E-05, 5.213463471025706227E-05, 6.641585710718375028E-05 ),
 .UNSPECIFIED. ) ;
#166092=DIRECTION ( 'NONE',  ( -1.000000000000000000, -1.646408749285562691E-14, 0.000000000000000000 ) ) ;
#166171=CARTESIAN_POINT ( 'NONE',  ( -16.77683809663752257, 9.950000000011138823, -188.3499999999999659 ) ) ;
#166331=SHAPE_REPRESENTATION_RELATIONSHIP ( 'NONE' , 'NONE' ,  #206680, #73277 ) ;
#166345=DIRECTION ( 'NONE',  ( -0.000000000000000000, 1.000000000000000000, -0.000000000000000000 ) ) ;
#166390=DIRECTION ( 'NONE',  ( 1.186688945009010077E-16, -1.000000000000000000, -0.000000000000000000 ) ) ;
#166438=EDGE_LOOP ( 'NONE', ( #152323, #197373, #111763, #24237, #21432, #213133, #197792, #245052, #86094, #76014, #165903, #52366, #204290, #233054 ) ) ;
#166549=DIRECTION ( 'NONE',  ( -1.186688945009010077E-16, 1.000000000000000000, 0.000000000000000000 ) ) ;
#166763=CARTESIAN_POINT ( 'NONE',  ( 18.39999999999999147, 8.822561741677553471, -176.7499999999999716 ) ) ;
#166923=EDGE_LOOP ( 'NONE', ( #186941, #255319, #77753, #216581, #228721, #193901 ) ) ;
#166978=( LENGTH_UNIT ( ) NAMED_UNIT ( * ) SI_UNIT ( .MILLI., .METRE. ) );
#167362=DIRECTION ( 'NONE',  ( 0.000000000000000000, 0.000000000000000000, 1.000000000000000000 ) ) ;
#167425=CARTESIAN_POINT ( 'NONE',  ( -23.25000000000000355, 5.650000000011139001, -188.3499999999999659 ) ) ;
#167478=CARTESIAN_POINT ( 'NONE',  ( -16.92209698673681473, 9.950000000011138823, -188.2893644329461438 ) ) ;
#167528=VERTEX_POINT ( 'NONE', #29420 ) ;
#167815=FACE_OUTER_BOUND ( 'NONE', #122650, .T. ) ;
#167886=EDGE_CURVE ( 'NONE', #54060, #141666, #150584, .T. ) ;
#167932=CARTESIAN_POINT ( 'NONE',  ( -15.75000000000000355, 9.350000000011140955, -184.2499999999999716 ) ) ;
#168068=PRODUCT ( 'Snap Open Cable Crossbars 6', 'Snap Open Cable Crossbars 6', '', ( #96462 ) ) ;
#168462=DIRECTION ( 'NONE',  ( -0.000000000000000000, 1.000000000000000000, 0.000000000000000000 ) ) ;
#168626=CARTESIAN_POINT ( 'NONE',  ( -16.81930730667006557, 9.936998068885200652, -180.2267677305381710 ) ) ;
#168904=AXIS2_PLACEMENT_3D ( 'NONE', #222919, #79547, #2586 ) ;
#168921=EDGE_CURVE ( 'NONE', #31330, #232305, #17832, .T. ) ;
#169199=DIRECTION ( 'NONE',  ( -1.020425574104004196E-15, 0.000000000000000000, 1.000000000000000000 ) ) ;
#169248=EDGE_CURVE ( 'NONE', #33770, #211794, #184846, .T. ) ;
#169346=VERTEX_POINT ( 'NONE', #148302 ) ;
#169348=EDGE_CURVE ( 'NONE', #111385, #56652, #130459, .T. ) ;
#169499=AXIS2_PLACEMENT_3D ( 'NONE', #7147, #25455, #243194 ) ;
#169510=LINE ( 'NONE', #209890, #147374 ) ;
#169547=CARTESIAN_POINT ( 'NONE',  ( -18.35668295345803713, 11.47316190337362940, -191.7499999999999716 ) ) ;
#169906=CARTESIAN_POINT ( 'NONE',  ( -16.87683809663753465, 9.864913778549569301, -180.7757156356384769 ) ) ;
#170070=EDGE_LOOP ( 'NONE', ( #163209, #132214, #232892, #45361, #229573 ) ) ;
#170208=AXIS2_PLACEMENT_3D ( 'NONE', #71817, #131768, #31426 ) ;
#170395=ORIENTED_EDGE ( 'NONE', *, *, #243595, .T. ) ;
#170760=CARTESIAN_POINT ( 'NONE',  ( -21.65000000000000213, 9.950000000011140600, -188.2499999999999716 ) ) ;
#170823=CARTESIAN_POINT ( 'NONE',  ( -16.83233564386404169, 9.930221796595755990, -180.2754793365243415 ) ) ;
#170840=CARTESIAN_POINT ( 'NONE',  ( -18.39418127959864790, 11.48390560170929220, -191.7499999999999716 ) ) ;
#171009=CARTESIAN_POINT ( 'NONE',  ( -16.89020380669786547, 9.950000000011137047, -180.2574111481105206 ) ) ;
#171146=AXIS2_PLACEMENT_3D ( 'NONE', #62122, #40018, #122096 ) ;
#171161=B_SPLINE_CURVE_WITH_KNOTS ( 'NONE', 3,
 ( #9148, #169547, #246467, #67827, #109511, #170840, #91256 ),
 .UNSPECIFIED., .F., .F.,
 ( 4, 3, 4 ),
 ( 0.000000000000000000, 3.882884552234471334E-05, 5.798605692158473166E-05 ),
 .UNSPECIFIED. ) ;
#171284=DIRECTION ( 'NONE',  ( -0.000000000000000000, -0.000000000000000000, -1.000000000000000000 ) ) ;
#171333=ORIENTED_EDGE ( 'NONE', *, *, #248831, .T. ) ;
#171464=AXIS2_PLACEMENT_3D ( 'NONE', #164429, #243948, #35217 ) ;
#171479=VERTEX_POINT ( 'NONE', #233703 ) ;
#171571=VERTEX_POINT ( 'NONE', #19796 ) ;
#171578=CARTESIAN_POINT ( 'NONE',  ( 14.22916352759893854, 9.457410930301318075, -185.9999159087462886 ) ) ;
#171625=AXIS2_PLACEMENT_3D ( 'NONE', #10013, #7435, #166549 ) ;
#171626=ORIENTED_EDGE ( 'NONE', *, *, #42233, .F. ) ;
#171694=VERTEX_POINT ( 'NONE', #143576 ) ;
#171786=CARTESIAN_POINT ( 'NONE',  ( -15.57281606413133090, 9.370655051134637148, -185.0258232559808675 ) ) ;
#171882=DIRECTION ( 'NONE',  ( -1.000000000000000000, -1.186688945009010077E-16, -0.000000000000000000 ) ) ;
#172151=CARTESIAN_POINT ( 'NONE',  ( -18.40000000000000213, 11.48667500176882861, -191.7499999999999716 ) ) ;
#172290=CARTESIAN_POINT ( 'NONE',  ( -16.81744102076749314, 9.950000000011142376, -180.1499999999999773 ) ) ;
#172378=ORIENTED_EDGE ( 'NONE', *, *, #29266, .T. ) ;
#172479=VERTEX_POINT ( 'NONE', #257713 ) ;
#172513=ADVANCED_FACE ( 'NONE', ( #85193 ), #65663, .F. ) ;
#172564=CARTESIAN_POINT ( 'NONE',  ( 17.74533788810829904, 10.81849979148194763, -190.6863773250524048 ) ) ;
#172889=DIRECTION ( 'NONE',  ( -1.000000000000000000, 0.000000000000000000, 0.000000000000000000 ) ) ;
#172992=VECTOR ( 'NONE', #123578, 1000.000000000000000 ) ;
#173083=CARTESIAN_POINT ( 'NONE',  ( -15.31895204843005232, 9.396533993965075382, -185.4059397791733090 ) ) ;
#173850=DIRECTION ( 'NONE',  ( 0.7071067811865474617, 0.7071067811865474617, 0.000000000000000000 ) ) ;
#173999=ORIENTED_EDGE ( 'NONE', *, *, #226229, .F. ) ;
#174153=CARTESIAN_POINT ( 'NONE',  ( -21.65000000000000213, 9.950000000011140600, -180.2499999999999716 ) ) ;
#174431=CARTESIAN_POINT ( 'NONE',  ( -18.40000000000000213, 5.650000000011139001, -180.1499999999999773 ) ) ;
#174704=DIRECTION ( 'NONE',  ( 0.000000000000000000, 0.000000000000000000, -1.000000000000000000 ) ) ;
#174721=( BOUNDED_SURFACE ( )  B_SPLINE_SURFACE ( 3, 2, ( 
 ( #17259, #96748, #255808 ),
 ( #77206, #177637, #78485 ),
 ( #198446, #219289, #236287 ),
 ( #19833, #158091, #99321 ),
 ( #178926, #79756, #159345 ),
 ( #40704, #120238, #127911 ),
 ( #87475, #105738, #226998 ),
 ( #242702, #7968, #88751 ),
 ( #125340, #246551, #224424 ),
 ( #108349, #23700, #26249 ) ),
 .UNSPECIFIED., .F., .F., .F. ) 
 B_SPLINE_SURFACE_WITH_KNOTS ( ( 4, 2, 2, 2, 4 ),
 ( 3, 3 ),
 ( 0.002161241639767248670, 0.002579950749615825267, 0.002789305304540113349, 0.002893982582002257390, 0.002998659859464401431 ),
 ( 0.000000000000000000, 1.000000000000000000 ),
 .UNSPECIFIED. ) 
 GEOMETRIC_REPRESENTATION_ITEM ( )  RATIONAL_B_SPLINE_SURFACE ( (
 ( 1.000000000000000000, 0.7071067811865536790, 1.000000000000000000),
 ( 1.000000000000000000, 0.7632447400667790038, 1.000000000000000000),
 ( 1.000000000000000000, 0.8158073005105432873, 1.000000000000000000),
 ( 1.000000000000000000, 0.8906973462398217745, 1.000000000000000000),
 ( 1.000000000000000000, 0.9149408947797255109, 1.000000000000000000),
 ( 1.000000000000000000, 0.9493368785277334077, 1.000000000000000000),
 ( 1.000000000000000000, 0.9605194247158570509, 1.000000000000000000),
 ( 1.000000000000000000, 0.9803630264779448211, 1.000000000000000000),
 ( 1.000000000000000000, 0.9900844824272494460, 1.000000000000000000),
 ( 1.000000000000000000, 0.9894588281429256282, 1.000000000000000000) ) ) 
 REPRESENTATION_ITEM ( '' )  SURFACE ( )  );
#174893=CARTESIAN_POINT ( 'NONE',  ( -18.40000000000000213, 11.47316190337364183, -191.6740539331919990 ) ) ;
#174932=ORIENTED_EDGE ( 'NONE', *, *, #20721, .F. ) ;
#175162=CARTESIAN_POINT ( 'NONE',  ( -12.25000000000000178, 9.850000000011133849, -184.2499999999999716 ) ) ;
#175628=DIRECTION ( 'NONE',  ( 0.000000000000000000, -1.000000000000000000, 0.000000000000000000 ) ) ;
#175812=LINE ( 'NONE', #255271, #143620 ) ;
#175891=( BOUNDED_CURVE ( )  B_SPLINE_CURVE ( 3, ( #13445, #92964, #172564, #252041 ),
 .UNSPECIFIED., .F., .F. ) 
 B_SPLINE_CURVE_WITH_KNOTS ( ( 4, 4 ),
 ( 3.432212674861196522, 3.693332928900581624 ),
 .UNSPECIFIED. ) 
 CURVE ( )  GEOMETRIC_REPRESENTATION_ITEM ( )  RATIONAL_B_SPLINE_CURVE ( ( 1.000000000000000000, 0.9943260843901261525, 0.9943260843901261525, 1.000000000000000000 ) ) 
 REPRESENTATION_ITEM ( '' )  );
#175908=AXIS2_PLACEMENT_3D ( 'NONE', #211982, #93295, #172889 ) ;
#176101=VECTOR ( 'NONE', #24522, 1000.000000000000000 ) ;
#176137=CARTESIAN_POINT ( 'NONE',  ( -16.94878442675512886, 9.991729103002160883, -188.3882195756378337 ) ) ;
#176295=CARTESIAN_POINT ( 'NONE',  ( -16.89060415895970735, 9.951220762813354881, -180.1459202242704123 ) ) ;
#176303=ADVANCED_FACE ( 'NONE', ( #178201 ), #25075, .T. ) ;
#176609=CYLINDRICAL_SURFACE ( 'NONE', #106922, 1.749999999999998002 ) ;
#177108=AXIS2_PLACEMENT_3D ( 'NONE', #247309, #49110, #208210 ) ;
#177122=ORIENTED_EDGE ( 'NONE', *, *, #155463, .F. ) ;
#177158=CARTESIAN_POINT ( 'NONE',  ( -16.85718274719485166, 9.976142314632857833, -180.0633463321825616 ) ) ;
#177280=CIRCLE ( 'NONE', #168904, 14.30833333333333890 ) ;
#177436=FACE_OUTER_BOUND ( 'NONE', #137383, .T. ) ;
#177637=CARTESIAN_POINT ( 'NONE',  ( -16.89155683852479228, 9.950000000011138823, -187.7226281504588599 ) ) ;
#177642=PLANE ( 'NONE',  #44494 ) ;
#177818=CARTESIAN_POINT ( 'NONE',  ( -18.40000000000000213, 11.47316190337362762, -180.1499999999999773 ) ) ;
#178140=ADVANCED_FACE ( 'NONE', ( #197158 ), #177642, .F. ) ;
#178201=FACE_OUTER_BOUND ( 'NONE', #241264, .T. ) ;
#178693=CARTESIAN_POINT ( 'NONE',  ( -16.88593481969334675, 9.950560090095464716, -188.3518722569444606 ) ) ;
#178926=CARTESIAN_POINT ( 'NONE',  ( -16.84981964351507600, 9.917318234109812281, -188.1303983859795892 ) ) ;
#179197=DIRECTION ( 'NONE',  ( 1.000000000000000000, 0.000000000000000000, 1.073024830501117725E-15 ) ) ;
#179230=CARTESIAN_POINT ( 'NONE',  ( 20.73486653747088937, 7.750000000011182166, -180.1499999999999773 ) ) ;
#179631=VECTOR ( 'NONE', #112827, 1000.000000000000000 ) ;
#179647=VERTEX_POINT ( 'NONE', #244868 ) ;
#179785=CARTESIAN_POINT ( 'NONE',  ( -16.87036670365549540, 9.989418819312804843, -180.0204398826979286 ) ) ;
#180104=CYLINDRICAL_SURFACE ( 'NONE', #37862, 1.749999999999998002 ) ;
#180120=VECTOR ( 'NONE', #59443, 1000.000000000000000 ) ;
#180388=EDGE_CURVE ( 'NONE', #114189, #129693, #154190, .T. ) ;
#180420=CARTESIAN_POINT ( 'NONE',  ( -23.25000000000000355, 5.650000000011139001, -176.7499999999999716 ) ) ;
#180894=CARTESIAN_POINT ( 'NONE',  ( -17.27223548804059661, 10.34539739140874381, -189.6336061792289627 ) ) ;
#180935=FACE_OUTER_BOUND ( 'NONE', #71952, .T. ) ;
#180988=CARTESIAN_POINT ( 'NONE',  ( -16.94389599337536012, 9.991197989767877985, -188.3923551982015852 ) ) ;
#181118=FACE_OUTER_BOUND ( 'NONE', #231119, .T. ) ;
#181150=ADVANCED_FACE ( 'NONE', ( #213495 ), #252618, .F. ) ;
#181235=LINE ( 'NONE', #196918, #124682 ) ;
#181248=DIRECTION ( 'NONE',  ( 1.000000000000000000, 0.000000000000000000, 0.000000000000000000 ) ) ;
#181393=FILL_AREA_STYLE_COLOUR ( '', #33007 ) ;
#181453=VECTOR ( 'NONE', #146480, 1000.000000000000000 ) ;
#181729=CARTESIAN_POINT ( 'NONE',  ( -14.11697426661281440, 9.457410944778571249, -182.5000839737900264 ) ) ;
#181948=AXIS2_PLACEMENT_3D ( 'NONE', #118535, #200617, #104052 ) ;
#181967=VERTEX_POINT ( 'NONE', #25932 ) ;
#182281=B_SPLINE_CURVE_WITH_KNOTS ( 'NONE', 3,
 ( #41402, #21824, #98742, #928, #140467, #160069, #137892, #120949, #80461, #222559 ),
 .UNSPECIFIED., .F., .F.,
 ( 4, 3, 3, 4 ),
 ( 7.632826238681696029E-06, 4.756916949875625587E-05, 9.484459048152062838E-05, 0.0001435500935100044199 ),
 .UNSPECIFIED. ) ;
#182493=EDGE_CURVE ( 'NONE', #47603, #172479, #127043, .T. ) ;
#182531=CARTESIAN_POINT ( 'NONE',  ( -16.88328101497759448, 9.950352834230013599, -188.3511795149292425 ) ) ;
#182668=SURFACE_SIDE_STYLE ('',( #223051 ) ) ;
#182684=EDGE_CURVE ( 'NONE', #4251, #185125, #214508, .T. ) ;
#182843=ORIENTED_EDGE ( 'NONE', *, *, #229768, .F. ) ;
#182871=CARTESIAN_POINT ( 'NONE',  ( -16.94107738177415712, 10.01423928514777728, -180.0499999999999545 ) ) ;
#182903=CARTESIAN_POINT ( 'NONE',  ( -16.87036670365549895, 9.989418819312803066, -180.0204398826979286 ) ) ;
#183219=CARTESIAN_POINT ( 'NONE',  ( 15.39793903038208533, 9.389686005666813884, -183.1728435063512848 ) ) ;
#183383=DIRECTION ( 'NONE',  ( -1.020425574104004196E-15, -1.210927747993693964E-31, -1.000000000000000000 ) ) ;
#183640=EDGE_CURVE ( 'NONE', #56614, #241870, #161798, .T. ) ;
#183746=EDGE_CURVE ( 'NONE', #248393, #433, #118470, .T. ) ;
#183818=CARTESIAN_POINT ( 'NONE',  ( -16.93388492042259230, 9.988541822527057690, -180.0994548768137804 ) ) ;
#183940=ORIENTED_EDGE ( 'NONE', *, *, #20721, .T. ) ;
#184015=CARTESIAN_POINT ( 'NONE',  ( -16.27683809663750480, 9.350000000011133849, -188.4499999999999886 ) ) ;
#184146=CARTESIAN_POINT ( 'NONE',  ( -17.01825945287481545, 9.950000000011138823, -188.2499999999999716 ) ) ;
#184172=CARTESIAN_POINT ( 'NONE',  ( 16.87683809663750267, 9.950000000011138823, -180.1499999999999773 ) ) ;
#184278=LINE ( 'NONE', #125591, #190143 ) ;
#184471=CARTESIAN_POINT ( 'NONE',  ( 18.39999999999999503, 5.650000000011139001, -188.3499999999999659 ) ) ;
#184478=CARTESIAN_POINT ( 'NONE',  ( 13.43443725621852813, 9.446557523083688679, -182.5899419543458464 ) ) ;
#184518=ORIENTED_EDGE ( 'NONE', *, *, #125197, .T. ) ;
#184792=FACE_OUTER_BOUND ( 'NONE', #101938, .T. ) ;
#184816=DIRECTION ( 'NONE',  ( 0.000000000000000000, 0.000000000000000000, 1.000000000000000000 ) ) ;
#184846=LINE ( 'NONE', #203131, #176101 ) ;
#184848=EDGE_LOOP ( 'NONE', ( #115874, #132701, #210074, #97250, #163673, #109017 ) ) ;
#184878=CARTESIAN_POINT ( 'NONE',  ( -16.94445028196808778, 9.992063609708889516, -180.1073301784184366 ) ) ;
#184954=DIRECTION ( 'NONE',  ( -0.000000000000000000, -0.000000000000000000, -1.000000000000000000 ) ) ;
#185125=VERTEX_POINT ( 'NONE', #229501 ) ;
#185145=CARTESIAN_POINT ( 'NONE',  ( -16.80469485234341320, 9.942151663152191787, -188.3099668439311074 ) ) ;
#185208=ORIENTED_EDGE ( 'NONE', *, *, #92779, .T. ) ;
#185435=EDGE_LOOP ( 'NONE', ( #238045, #136433, #10291 ) ) ;
#185487=ORIENTED_EDGE ( 'NONE', *, *, #1875, .F. ) ;
#185621=CARTESIAN_POINT ( 'NONE',  ( 20.73486653747088582, 7.250000000011182166, -176.7499999999999716 ) ) ;
#185871=ADVANCED_FACE ( 'NONE', ( #4669 ), #65951, .F. ) ;
#185891=CARTESIAN_POINT ( 'NONE',  ( 23.04999999999999716, 8.822561741677553471, -191.7499999999999716 ) ) ;
#186086=PLANE ( 'NONE',  #171625 ) ;
#186398=CARTESIAN_POINT ( 'NONE',  ( -16.92132318717937522, 9.966070024017081863, -180.1224066303520317 ) ) ;
#186512=( NAMED_UNIT ( * ) SI_UNIT ( $, .STERADIAN. ) SOLID_ANGLE_UNIT ( ) );
#186941=ORIENTED_EDGE ( 'NONE', *, *, #128877, .T. ) ;
#187058=ORIENTED_EDGE ( 'NONE', *, *, #169348, .T. ) ;
#187162=LINE ( 'NONE', #100195, #127684 ) ;
#187164=( NAMED_UNIT ( * ) SI_UNIT ( $, .STERADIAN. ) SOLID_ANGLE_UNIT ( ) );
#187245=CARTESIAN_POINT ( 'NONE',  ( -17.22361732159832215, 10.34515565861359221, -178.8707845258671227 ) ) ;
#187282=VECTOR ( 'NONE', #175628, 1000.000000000000000 ) ;
#187437=EDGE_CURVE ( 'NONE', #167528, #220874, #197097, .T. ) ;
#187460=CARTESIAN_POINT ( 'NONE',  ( -20.65000000000000568, 7.250000000011138646, -188.3499999999999659 ) ) ;
#187482=CARTESIAN_POINT ( 'NONE',  ( -13.54036565897076727, 9.451541661396669625, -185.9538754988305698 ) ) ;
#187687=CARTESIAN_POINT ( 'NONE',  ( -16.92925196614876171, 9.972331796421276096, -180.1167448477167454 ) ) ;
#187746=VECTOR ( 'NONE', #96792, 1000.000000000000000 ) ;
#187778=CARTESIAN_POINT ( 'NONE',  ( -16.80891096016330621, 9.950000000011137047, -180.1323371927318533 ) ) ;
#188093=PLANE ( 'NONE',  #204705 ) ;
#188529=ORIENTED_EDGE ( 'NONE', *, *, #141005, .F. ) ;
#188724=PLANE ( 'NONE',  #147753 ) ;
#188781=ORIENTED_EDGE ( 'NONE', *, *, #126284, .F. ) ;
#188809=CARTESIAN_POINT ( 'NONE',  ( -17.04761207306817639, 10.02645087340892438, -188.3499999999999943 ) ) ;
#188831=( BOUNDED_SURFACE ( )  B_SPLINE_SURFACE ( 3, 2, ( 
 ( #224015, #199346, #200618 ),
 ( #85759, #222729, #124937 ),
 ( #84466, #204450, #100198 ),
 ( #25837, #119817, #179785 ) ),
 .UNSPECIFIED., .F., .F., .T. ) 
 B_SPLINE_SURFACE_WITH_KNOTS ( ( 4, 4 ),
 ( 3, 3 ),
 ( 5.727910411845712702, 5.983100554402350113 ),
 ( 0.000000000000000000, 1.000000000000000000 ),
 .UNSPECIFIED. ) 
 GEOMETRIC_REPRESENTATION_ITEM ( )  RATIONAL_B_SPLINE_SURFACE ( (
 ( 1.000000000000000000, 0.8946697475931897348, 1.000000000000000000),
 ( 1.000000000000000000, 0.9035312726221080837, 1.000000000000000000),
 ( 1.000000000000000000, 0.9104333467450060891, 1.000000000000000000),
 ( 1.000000000000000000, 0.9152888060719425178, 1.000000000000000000) ) ) 
 REPRESENTATION_ITEM ( '' )  SURFACE ( )  );
#188951=CARTESIAN_POINT ( 'NONE',  ( -16.93658623642901873, 9.980381671668284937, -180.1119027291291559 ) ) ;
#189000=VERTEX_POINT ( 'NONE', #212665 ) ;
#189001=CARTESIAN_POINT ( 'NONE',  ( -16.78493211734304680, 9.945835743215326374, -188.3360509808959762 ) ) ;
#189034=ORIENTED_EDGE ( 'NONE', *, *, #167886, .F. ) ;
#189103=ORIENTED_EDGE ( 'NONE', *, *, #56287, .T. ) ;
#189245=CARTESIAN_POINT ( 'NONE',  ( -16.94225986326250322, 9.950000000011138823, -180.4467193756078416 ) ) ;
#189277=CARTESIAN_POINT ( 'NONE',  ( -18.40000000000000213, 11.48667500176882861, -191.7499999999999716 ) ) ;
#189341=DIRECTION ( 'NONE',  ( -1.000000000000000000, 0.000000000000000000, 0.000000000000000000 ) ) ;
#189795=CARTESIAN_POINT ( 'NONE',  ( -17.71734398241073905, 10.84235722847571814, -177.7748617469943611 ) ) ;
#189808=ORIENTED_EDGE ( 'NONE', *, *, #144447, .F. ) ;
#189830=CARTESIAN_POINT ( 'NONE',  ( 13.22461703343585349, 9.436662931810245070, -185.8230367322949235 ) ) ;
#189958=CARTESIAN_POINT ( 'NONE',  ( -16.89268316805465986, 9.951721813253337601, -188.3557524785454973 ) ) ;
#189993=ADVANCED_FACE ( 'NONE', ( #86294 ), #130574, .F. ) ;
#190032=CARTESIAN_POINT ( 'NONE',  ( -12.68215100488890634, 9.396630376328873879, -185.4070573928183023 ) ) ;
#190133=CARTESIAN_POINT ( 'NONE',  ( -16.87683809663752399, 23.65833333334447985, -184.2499999999999716 ) ) ;
#190143=VECTOR ( 'NONE', #22670, 1000.000000000000000 ) ;
#190384=( BOUNDED_CURVE ( )  B_SPLINE_CURVE ( 3, ( #144122, #45044, #122016, #202830 ),
 .UNSPECIFIED., .F., .T. ) 
 B_SPLINE_CURVE_WITH_KNOTS ( ( 4, 4 ),
 ( 1.570796326794908992, 2.617993877991413587 ),
 .UNSPECIFIED. ) 
 CURVE ( )  GEOMETRIC_REPRESENTATION_ITEM ( )  RATIONAL_B_SPLINE_CURVE ( ( 1.000000000000000000, 0.9106836025229745335, 0.9106836025229745335, 1.000000000000000000 ) ) 
 REPRESENTATION_ITEM ( '' )  );
#190492=VERTEX_POINT ( 'NONE', #214950 ) ;
#190597=DIRECTION ( 'NONE',  ( -0.000000000000000000, 1.000000000000000000, 0.000000000000000000 ) ) ;
#190830=LINE ( 'NONE', #92969, #37730 ) ;
#190834=CARTESIAN_POINT ( 'NONE',  ( -23.25000000000000355, 5.650000000011139001, -180.1499999999999773 ) ) ;
#190867=CLOSED_SHELL ( 'NONE', ( #225451, #194907, #73982, #257478, #185871, #111415, #181150, #60140, #109057, #235634, #158075, #62580, #13006, #252021, #42842, #178140, #108398, #134167, #138258, #114437, #172513, #16364, #98542, #9610, #222313, #33946, #148253, #203896, #240164, #109934, #189993, #64232, #227119, #194534, #133842, #252176, #58894, #52575, #99638, #176303, #4770, #33184, #257677, #205680, #10914, #45355, #74459, #195900, #137402, #250812, #102664, #48223, #69092 ) ) ;
#191004=DIRECTION ( 'NONE',  ( 1.000000000000000000, -0.000000000000000000, -0.000000000000000000 ) ) ;
#191010=CIRCLE ( 'NONE', #207756, 1.749999999999998002 ) ;
#191235=MANIFOLD_SOLID_BREP ( 'Stock-MAS-200-1', #190867 ) ;
#191345=CARTESIAN_POINT ( 'NONE',  ( -14.45422546970483957, 9.450602096099679272, -185.9438959630966792 ) ) ;
#191835=CARTESIAN_POINT ( 'NONE',  ( -16.86132326855786090, 9.950000000011137047, -180.1986357846682836 ) ) ;
#191849=EDGE_CURVE ( 'NONE', #239382, #195448, #196447, .T. ) ;
#191979=ORIENTED_EDGE ( 'NONE', *, *, #164098, .F. ) ;
#192332=ORIENTED_EDGE ( 'NONE', *, *, #207088, .F. ) ;
#192392=CARTESIAN_POINT ( 'NONE',  ( -21.65000000000000213, 7.250000000011138646, -180.1499999999999773 ) ) ;
#192472=DIRECTION ( 'NONE',  ( 1.000000000000000000, 0.000000000000000000, 0.000000000000000000 ) ) ;
#192553=EDGE_LOOP ( 'NONE', ( #123234, #10084, #122318, #48328 ) ) ;
#192577=VERTEX_POINT ( 'NONE', #256737 ) ;
#192639=EDGE_CURVE ( 'NONE', #77200, #56652, #25897, .T. ) ;
#192989=CARTESIAN_POINT ( 'NONE',  ( -16.97683809663752186, 9.950000000011138823, -187.5976359818036485 ) ) ;
#193031=ORIENTED_EDGE ( 'NONE', *, *, #71531, .F. ) ;
#193090=VECTOR ( 'NONE', #39815, 1000.000000000000000 ) ;
#193276=CARTESIAN_POINT ( 'NONE',  ( -16.87331047859651179, 9.950000000011142376, -180.1499999999999773 ) ) ;
#193531=ORIENTED_EDGE ( 'NONE', *, *, #86065, .T. ) ;
#193808=DIRECTION ( 'NONE',  ( 0.000000000000000000, 0.000000000000000000, -1.000000000000000000 ) ) ;
#193901=ORIENTED_EDGE ( 'NONE', *, *, #13690, .T. ) ;
#194329=DIRECTION ( 'NONE',  ( -0.000000000000000000, -0.000000000000000000, -1.000000000000000000 ) ) ;
#194418=CARTESIAN_POINT ( 'NONE',  ( -16.91256925476569961, 9.985731158139330432, -188.4676424890052431 ) ) ;
#194534=ADVANCED_FACE ( 'NONE', ( #35472 ), #188093, .T. ) ;
#194635=DIRECTION ( 'NONE',  ( 0.000000000000000000, 0.000000000000000000, 1.000000000000000000 ) ) ;
#194674=ORIENTED_EDGE ( 'NONE', *, *, #252724, .T. ) ;
#194705=LINE ( 'NONE', #175162, #136202 ) ;
#194791=ORIENTED_EDGE ( 'NONE', *, *, #116492, .T. ) ;
#194813=EDGE_CURVE ( 'NONE', #4251, #2708, #40068, .T. ) ;
#194907=ADVANCED_FACE ( 'NONE', ( #63435 ), #103834, .F. ) ;
#195113=FACE_OUTER_BOUND ( 'NONE', #11818, .T. ) ;
#195175=ORIENTED_EDGE ( 'NONE', *, *, #77069, .T. ) ;
#195423=DIRECTION ( 'NONE',  ( -0.000000000000000000, -0.000000000000000000, -1.000000000000000000 ) ) ;
#195448=VERTEX_POINT ( 'NONE', #164819 ) ;
#195552=ORIENTED_EDGE ( 'NONE', *, *, #100642, .F. ) ;
#195610=CARTESIAN_POINT ( 'NONE',  ( -16.80939487329395021, 9.950000000011138823, -188.3500000000008470 ) ) ;
#195800=PLANE ( 'NONE',  #226743 ) ;
#195900=ADVANCED_FACE ( 'NONE', ( #84930 ), #121567, .T. ) ;
#196094=CARTESIAN_POINT ( 'NONE',  ( -16.93433913041102912, 10.00597842153509376, -188.4353654273951406 ) ) ;
#196310=CARTESIAN_POINT ( 'NONE',  ( 23.24999999999999645, 11.75000000001113953, -180.1499999999999773 ) ) ;
#196314=DIRECTION ( 'NONE',  ( 0.000000000000000000, 0.000000000000000000, 1.000000000000000000 ) ) ;
#196447=LINE ( 'NONE', #213448, #187282 ) ;
#196705=ORIENTED_EDGE ( 'NONE', *, *, #169348, .F. ) ;
#196918=CARTESIAN_POINT ( 'NONE',  ( -15.55912972643741199, 8.490870273573719373, -180.1499999999999773 ) ) ;
#196939=DIRECTION ( 'NONE',  ( 0.5932847527679299127, -0.8049926720990051576, 6.366092712777055223E-16 ) ) ;
#197097=( BOUNDED_CURVE ( )  B_SPLINE_CURVE ( 3, ( #35596, #255842, #52543, #132098 ),
 .UNSPECIFIED., .F., .F. ) 
 B_SPLINE_CURVE_WITH_KNOTS ( ( 4, 4 ),
 ( 0.3000847527772385614, 0.5517402753107881752 ),
 .UNSPECIFIED. ) 
 CURVE ( )  GEOMETRIC_REPRESENTATION_ITEM ( )  RATIONAL_B_SPLINE_CURVE ( ( 1.000000000000000000, 0.9947294176030464508, 0.9947294176030464508, 1.000000000000000000 ) ) 
 REPRESENTATION_ITEM ( '' )  );
#197158=FACE_OUTER_BOUND ( 'NONE', #90116, .T. ) ;
#197207=DIRECTION ( 'NONE',  ( 1.000000000000000000, 1.646408749285562691E-14, 1.073024830501117725E-15 ) ) ;
#197363=CARTESIAN_POINT ( 'NONE',  ( -16.93589915522259304, 10.00862525870701347, -188.4405601019602727 ) ) ;
#197373=ORIENTED_EDGE ( 'NONE', *, *, #128136, .F. ) ;
#197496=DIRECTION ( 'NONE',  ( -1.000000000000000000, 0.000000000000000000, 0.000000000000000000 ) ) ;
#197705=VECTOR ( 'NONE', #197870, 1000.000000000000000 ) ;
#197720=PLANE ( 'NONE',  #38054 ) ;
#197745=CARTESIAN_POINT ( 'NONE',  ( 16.87683809663749557, 9.950000000011131718, -188.3499999999999659 ) ) ;
#197792=ORIENTED_EDGE ( 'NONE', *, *, #126126, .F. ) ;
#197832=( BOUNDED_SURFACE ( )  B_SPLINE_SURFACE ( 3, 2, ( 
 ( #63968, #142211, #62688 ),
 ( #82205, #83490, #61395 ),
 ( #140947, #26135, #220485 ),
 ( #121411, #200906, #101768 ),
 ( #2691, #112097, #91240 ),
 ( #10419, #49538, #170823 ),
 ( #32580, #131636, #92502 ),
 ( #232044, #226882, #129080 ),
 ( #187778, #250301, #110786 ),
 ( #48248, #206044, #9131 ) ),
 .UNSPECIFIED., .F., .F., .F. ) 
 B_SPLINE_SURFACE_WITH_KNOTS ( ( 4, 2, 2, 2, 4 ),
 ( 3, 3 ),
 ( 0.002161241639767785133, 0.002579950749617447234, 0.002789305304542278284, 0.002893982582004694243, 0.002998659859467109768 ),
 ( 0.000000000000000000, 1.000000000000000000 ),
 .UNSPECIFIED. ) 
 GEOMETRIC_REPRESENTATION_ITEM ( )  RATIONAL_B_SPLINE_SURFACE ( (
 ( 1.000000000000000000, 0.7071067811864923947, 1.000000000000000000),
 ( 1.000000000000000000, 0.7632447400664396087, 1.000000000000000000),
 ( 1.000000000000000000, 0.8158073005108742448, 1.000000000000000000),
 ( 1.000000000000000000, 0.8906973462396178265, 1.000000000000000000),
 ( 1.000000000000000000, 0.9149408947802133429, 1.000000000000000000),
 ( 1.000000000000000000, 0.9493368785274678423, 1.000000000000000000),
 ( 1.000000000000000000, 0.9605194247157190501, 1.000000000000000000),
 ( 1.000000000000000000, 0.9803630264780686110, 1.000000000000000000),
 ( 1.000000000000000000, 0.9900844824271547440, 1.000000000000000000),
 ( 1.000000000000000000, 0.9894588281429235188, 1.000000000000000000) ) ) 
 REPRESENTATION_ITEM ( '' )  SURFACE ( )  );
#197870=DIRECTION ( 'NONE',  ( 1.000000000000000000, -0.000000000000000000, -0.000000000000000000 ) ) ;
#198009=ORIENTED_EDGE ( 'NONE', *, *, #27587, .F. ) ;
#198145=CARTESIAN_POINT ( 'NONE',  ( -16.80117486205003630, 9.949657268323468529, -188.3488548729254717 ) ) ;
#198240=CARTESIAN_POINT ( 'NONE',  ( 16.27683809663750125, 9.350000000011137402, -176.7499999999999716 ) ) ;
#198366=DIRECTION ( 'NONE',  ( 1.000000000000000000, 0.000000000000000000, 0.000000000000000000 ) ) ;
#198446=CARTESIAN_POINT ( 'NONE',  ( -16.87333278164157946, 9.882609784590092872, -187.8668321938465056 ) ) ;
#198901=ORIENTED_EDGE ( 'NONE', *, *, #141005, .T. ) ;
#199346=CARTESIAN_POINT ( 'NONE',  ( -18.41431012584569871, 11.48747202921931709, -176.7267639868983338 ) ) ;
#199357=LINE ( 'NONE', #55954, #157112 ) ;
#199457=CARTESIAN_POINT ( 'NONE',  ( -16.77779411440718249, 9.946101447118758543, -188.3369425829954480 ) ) ;
#199640=CARTESIAN_POINT ( 'NONE',  ( -18.40000000000000213, 5.650000000011139001, -180.1499999999999773 ) ) ;
#200064=AXIS2_PLACEMENT_3D ( 'NONE', #174431, #72747, #153583 ) ;
#200123=DIRECTION ( 'NONE',  ( -0.000000000000000000, -0.000000000000000000, -1.000000000000000000 ) ) ;
#200259=CARTESIAN_POINT ( 'NONE',  ( -33.72168855820451938, 9.950000000011156587, -180.1499999999999204 ) ) ;
#200609=CARTESIAN_POINT ( 'NONE',  ( 20.99999999999999645, 9.750000000011137757, -188.3499999999999659 ) ) ;
#200617=DIRECTION ( 'NONE',  ( 0.2834754621636358940, -0.2834754621636437211, 0.9161240771326893961 ) ) ;
#200618=CARTESIAN_POINT ( 'NONE',  ( -18.37013991200266005, 11.49974761622312691, -176.7069769894828539 ) ) ;
#200792=CARTESIAN_POINT ( 'NONE',  ( 21.72449340488910252, 10.28395627750227703, -180.1499999999999773 ) ) ;
#200801=CARTESIAN_POINT ( 'NONE',  ( -14.00000000000000178, 9.850000000011133849, -184.2499999999999716 ) ) ;
#200906=CARTESIAN_POINT ( 'NONE',  ( -16.88705144915419964, 9.950000000011137047, -180.4309785947120020 ) ) ;
#200921=DIRECTION ( 'NONE',  ( -0.000000000000000000, 1.000000000000000000, -0.000000000000000000 ) ) ;
#201281=CARTESIAN_POINT ( 'NONE',  ( -12.60206096961792177, 9.389686005666810331, -183.1728435063512848 ) ) ;
#201397=CARTESIAN_POINT ( 'NONE',  ( -18.40000000000000213, 11.75000000001113953, -180.1499999999999773 ) ) ;
#201597=ORIENTED_EDGE ( 'NONE', *, *, #98097, .T. ) ;
#201892=DIRECTION ( 'NONE',  ( 1.073024830501117725E-15, -0.000000000000000000, -1.000000000000000000 ) ) ;
#202063=ORIENTED_EDGE ( 'NONE', *, *, #180388, .T. ) ;
#202496=CARTESIAN_POINT ( 'NONE',  ( -16.87683809663752399, 9.850000000011140955, -180.1499999999999773 ) ) ;
#202746=EDGE_CURVE ( 'NONE', #129693, #86347, #149440, .T. ) ;
#202768=CARTESIAN_POINT ( 'NONE',  ( 12.60053434924910754, 9.389534562357859215, -183.1748093043899530 ) ) ;
#202830=CARTESIAN_POINT ( 'NONE',  ( -16.87331047859649757, 9.950000000011138823, -188.3499999999999659 ) ) ;
#203131=CARTESIAN_POINT ( 'NONE',  ( -21.65000000000000213, 9.950000000011140600, -180.1499999999999773 ) ) ;
#203485=ORIENTED_EDGE ( 'NONE', *, *, #71887, .F. ) ;
#203896=ADVANCED_FACE ( 'NONE', ( #66944 ), #12139, .F. ) ;
#204092=ORIENTED_EDGE ( 'NONE', *, *, #236961, .F. ) ;
#204244=ORIENTED_EDGE ( 'NONE', *, *, #66794, .F. ) ;
#204290=ORIENTED_EDGE ( 'NONE', *, *, #237508, .F. ) ;
#204378=EDGE_LOOP ( 'NONE', ( #195175, #158876, #52976, #100616, #223262 ) ) ;
#204450=CARTESIAN_POINT ( 'NONE',  ( -17.27223548801929454, 10.34539739139951209, -178.8663938208082413 ) ) ;
#204542=DIRECTION ( 'NONE',  ( -1.000000000000000000, 1.652117596168391700E-15, 0.000000000000000000 ) ) ;
#204650=CARTESIAN_POINT ( 'NONE',  ( -16.95709691156899268, 9.950000000010779999, -180.1600575625135150 ) ) ;
#204686=DIRECTION ( 'NONE',  ( -1.652117596168391700E-15, -1.000000000000000000, 0.000000000000000000 ) ) ;
#204705=AXIS2_PLACEMENT_3D ( 'NONE', #88967, #210240, #249360 ) ;
#204731=CARTESIAN_POINT ( 'NONE',  ( -16.79184697841823848, 9.948761661669548673, -180.1541422706025060 ) ) ;
#204994=CARTESIAN_POINT ( 'NONE',  ( -16.86422026484316916, 9.970447360871808939, -180.0822132256729731 ) ) ;
#205184=EDGE_CURVE ( 'NONE', #171694, #13123, #190830, .T. ) ;
#205315=CARTESIAN_POINT ( 'NONE',  ( 13.22261339317536866, 9.436552840015581367, -182.6779554727603738 ) ) ;
#205680=ADVANCED_FACE ( 'NONE', ( #228655 ), #130811, .F. ) ;
#205750=EDGE_CURVE ( 'NONE', #107596, #232238, #60255, .T. ) ;
#206044=CARTESIAN_POINT ( 'NONE',  ( -16.77308656112214535, 9.950000000011142376, -180.1501931917022716 ) ) ;
#206111=EDGE_LOOP ( 'NONE', ( #226876, #102330, #26085, #16224 ) ) ;
#206219=( BOUNDED_SURFACE ( )  B_SPLINE_SURFACE ( 3, 2, ( 
 ( #242134, #101290, #144295 ),
 ( #83031, #180894, #45225 ),
 ( #62229, #143017, #141749 ),
 ( #23120, #222557, #221277 ) ),
 .UNSPECIFIED., .F., .F., .F. ) 
 B_SPLINE_SURFACE_WITH_KNOTS ( ( 4, 4 ),
 ( 3, 3 ),
 ( 0.3000847527772371737, 0.5552748953338753068 ),
 ( 0.000000000000000000, 1.000000000000000000 ),
 .UNSPECIFIED. ) 
 GEOMETRIC_REPRESENTATION_ITEM ( )  RATIONAL_B_SPLINE_SURFACE ( (
 ( 1.000000000000000000, 0.9152888060719498453, 1.000000000000000000),
 ( 1.000000000000000000, 0.9104333467450272943, 1.000000000000000000),
 ( 1.000000000000000000, 0.9035312726220395829, 1.000000000000000000),
 ( 1.000000000000000000, 0.8946697475932223753, 1.000000000000000000) ) ) 
 REPRESENTATION_ITEM ( '' )  SURFACE ( )  );
#206299=FACE_OUTER_BOUND ( 'NONE', #74674, .T. ) ;
#206680=SHAPE_REPRESENTATION ( 'Snap Open Cable Crossbars 6', ( #2425 ), #131439 ) ;
#206812=DIRECTION ( 'NONE',  ( 1.186688945009010077E-16, -1.000000000000000000, -0.000000000000000000 ) ) ;
#206832=CARTESIAN_POINT ( 'NONE',  ( -16.97683809663752186, 9.950000000011138823, -187.5976359818036485 ) ) ;
#206901=B_SPLINE_CURVE_WITH_KNOTS ( 'NONE', 3,
 ( #60096, #114952, #57524, #254434, #79654, #95389, #90560, #135782, #137082, #216614, #139623, #40590, #116253, #237469, #118819, #78379, #96637, #17159, #255697 ),
 .UNSPECIFIED., .F., .F.,
 ( 4, 3, 3, 3, 3, 3, 4 ),
 ( 0.0001624081864585664764, 0.0001685232196531825368, 0.0001764526673566942224, 0.0001916878551483208173, 0.0002009890782182613455, 0.0002238845907555189795, 0.0002283406619926576847 ),
 .UNSPECIFIED. ) ;
#207088=EDGE_CURVE ( 'NONE', #218279, #222610, #230345, .T. ) ;
#207175=CIRCLE ( 'NONE', #61231, 0.9000000000000014655 ) ;
#207181=CARTESIAN_POINT ( 'NONE',  ( 18.39999999999999503, 11.75000000001113953, -180.1499999999999773 ) ) ;
#207255=FACE_OUTER_BOUND ( 'NONE', #119734, .T. ) ;
#207469=ORIENTED_EDGE ( 'NONE', *, *, #109384, .F. ) ;
#207531=CARTESIAN_POINT ( 'NONE',  ( -16.90137573187933384, 9.950000000011137047, -180.2884174240968775 ) ) ;
#207553=CARTESIAN_POINT ( 'NONE',  ( -16.87036670365548474, 9.989418819312801290, -188.4795601173020145 ) ) ;
#207756=AXIS2_PLACEMENT_3D ( 'NONE', #147410, #7917, #246504 ) ;
#207813=ORIENTED_EDGE ( 'NONE', *, *, #236939, .F. ) ;
#207924=FACE_OUTER_BOUND ( 'NONE', #84370, .T. ) ;
#207969=ORIENTED_EDGE ( 'NONE', *, *, #233623, .F. ) ;
#208210=DIRECTION ( 'NONE',  ( 1.000000000000000000, 1.186688945009009831E-16, 0.000000000000000000 ) ) ;
#208364=CARTESIAN_POINT ( 'NONE',  ( 20.27550659511089037, 9.216043722520002035, -180.1499999999999773 ) ) ;
#208581=CARTESIAN_POINT ( 'NONE',  ( -16.79140778683509438, 9.944941598865719712, -188.3297372337707714 ) ) ;
#208610=DIRECTION ( 'NONE',  ( -0.000000000000000000, 1.000000000000000000, -0.000000000000000000 ) ) ;
#208620=EDGE_LOOP ( 'NONE', ( #49556, #137665 ) ) ;
#208632=ORIENTED_EDGE ( 'NONE', *, *, #113216, .F. ) ;
#208804=ORIENTED_EDGE ( 'NONE', *, *, #254777, .T. ) ;
#209034=ORIENTED_EDGE ( 'NONE', *, *, #211512, .F. ) ;
#209342=ORIENTED_EDGE ( 'NONE', *, *, #39602, .F. ) ;
#209514=EDGE_CURVE ( 'NONE', #192577, #22307, #79501, .T. ) ;
#209890=CARTESIAN_POINT ( 'NONE',  ( 23.24999999999999645, 5.650000000011139001, -188.3499999999999659 ) ) ;
#210074=ORIENTED_EDGE ( 'NONE', *, *, #56654, .T. ) ;
#210107=CARTESIAN_POINT ( 'NONE',  ( -18.39999999999999858, 11.47316190337363828, -176.7998292484659544 ) ) ;
#210140=DIRECTION ( 'NONE',  ( -1.073024830501117725E-15, 0.000000000000000000, -1.000000000000000000 ) ) ;
#210240=DIRECTION ( 'NONE',  ( 1.186688945009009831E-16, -1.000000000000000000, 0.000000000000000000 ) ) ;
#210365=CARTESIAN_POINT ( 'NONE',  ( -15.55912972643741199, 8.490870273573719373, -180.0499999999999545 ) ) ;
#210487=EDGE_LOOP ( 'NONE', ( #94676, #233388, #39145, #142697 ) ) ;
#210719=DIRECTION ( 'NONE',  ( -0.000000000000000000, -0.000000000000000000, -1.000000000000000000 ) ) ;
#210780=AXIS2_PLACEMENT_3D ( 'NONE', #245010, #28590, #108080 ) ;
#210900=( BOUNDED_CURVE ( )  B_SPLINE_CURVE ( 3, ( #230197, #189795, #187245, #52832 ),
 .UNSPECIFIED., .F., .F. ) 
 B_SPLINE_CURVE_WITH_KNOTS ( ( 4, 4 ),
 ( 5.731445031868799056, 5.983100554402348337 ),
 .UNSPECIFIED. ) 
 CURVE ( )  GEOMETRIC_REPRESENTATION_ITEM ( )  RATIONAL_B_SPLINE_CURVE ( ( 1.000000000000000000, 0.9947294176030464508, 0.9947294176030464508, 1.000000000000000000 ) ) 
 REPRESENTATION_ITEM ( '' )  );
#211397=CARTESIAN_POINT ( 'NONE',  ( 20.09999999999999787, 9.750000000011137757, -188.3499999999999659 ) ) ;
#211479=VECTOR ( 'NONE', #46571, 1000.000000000000000 ) ;
#211498=EDGE_LOOP ( 'NONE', ( #189103, #143072 ) ) ;
#211512=EDGE_CURVE ( 'NONE', #42862, #247233, #240812, .T. ) ;
#211726=LINE ( 'NONE', #93039, #109347 ) ;
#211794=VERTEX_POINT ( 'NONE', #174153 ) ;
#211837=CARTESIAN_POINT ( 'NONE',  ( -18.40000000000000213, 5.650000000011139001, -188.3499999999999659 ) ) ;
#211972=CARTESIAN_POINT ( 'NONE',  ( 13.88638282980484284, 9.457426452500056868, -186.0000418683999897 ) ) ;
#211982=CARTESIAN_POINT ( 'NONE',  ( 20.04999999999999716, 8.750000000011173285, -176.7499999999999716 ) ) ;
#212175=CARTESIAN_POINT ( 'NONE',  ( -15.75000000000001066, 9.350000000011142731, -184.3642676076160853 ) ) ;
#212405=ORIENTED_EDGE ( 'NONE', *, *, #159680, .T. ) ;
#212416=FACE_OUTER_BOUND ( 'NONE', #137678, .T. ) ;
#212559=CARTESIAN_POINT ( 'NONE',  ( -16.90138253750126651, 9.950000000011137047, -188.2115627079045339 ) ) ;
#212665=CARTESIAN_POINT ( 'NONE',  ( -18.40000000000000213, 11.33174054713631662, -180.1499999999999773 ) ) ;
#213041=ORIENTED_EDGE ( 'NONE', *, *, #159690, .F. ) ;
#213133=ORIENTED_EDGE ( 'NONE', *, *, #163862, .F. ) ;
#213311=CARTESIAN_POINT ( 'NONE',  ( -16.97683809663752186, 9.850000000011140955, -180.1499999999999773 ) ) ;
#213448=CARTESIAN_POINT ( 'NONE',  ( 18.39999999999999503, 8.822561741677553471, -191.7499999999999716 ) ) ;
#213495=FACE_OUTER_BOUND ( 'NONE', #94747, .T. ) ;
#213599=EDGE_CURVE ( 'NONE', #232238, #235554, #153605, .T. ) ;
#213650=VECTOR ( 'NONE', #49775, 1000.000000000000000 ) ;
#213958=CARTESIAN_POINT ( 'NONE',  ( -16.92778301347360426, 10.00094491684723685, -188.4285181079673350 ) ) ;
#214291=CARTESIAN_POINT ( 'NONE',  ( 20.27550659511088682, 9.216043722520002035, -180.1499999999999773 ) ) ;
#214351=CARTESIAN_POINT ( 'NONE',  ( -18.40000000000000213, 11.47316190337364183, -191.7499999999999716 ) ) ;
#214366=CARTESIAN_POINT ( 'NONE',  ( -16.93234230245721861, 9.998107370558241058, -188.4176902816662107 ) ) ;
#214508=LINE ( 'NONE', #192392, #117025 ) ;
#214629=COLOUR_RGB ( '', 0.09019608, 0.27058824, 0.51372549) ;
#214820=VECTOR ( 'NONE', #111712, 1000.000000000000000 ) ;
#214950=CARTESIAN_POINT ( 'NONE',  ( -18.40000000000000213, 11.47316190337364183, -191.6740539331919990 ) ) ;
#215016=EDGE_LOOP ( 'NONE', ( #191979, #220363, #219577 ) ) ;
#215070=DIRECTION ( 'NONE',  ( 0.000000000000000000, 0.000000000000000000, 1.000000000000000000 ) ) ;
#215103=FACE_OUTER_BOUND ( 'NONE', #215016, .T. ) ;
#216330=CARTESIAN_POINT ( 'NONE',  ( -16.87683809663752399, 9.850000000011144508, -180.9023640181962662 ) ) ;
#216436=VECTOR ( 'NONE', #155469, 1000.000000000000000 ) ;
#216581=ORIENTED_EDGE ( 'NONE', *, *, #256129, .T. ) ;
#216614=CARTESIAN_POINT ( 'NONE',  ( -16.93255653858138388, 9.998451453988312920, -180.0816433679896420 ) ) ;
#216639=EDGE_CURVE ( 'NONE', #239382, #30570, #1384, .T. ) ;
#216857=EDGE_CURVE ( 'NONE', #247233, #96530, #169510, .T. ) ;
#216914=ORIENTED_EDGE ( 'NONE', *, *, #216639, .F. ) ;
#216923=CARTESIAN_POINT ( 'NONE',  ( 20.73486653747088582, 7.250000000011182166, -180.1499999999999773 ) ) ;
#217420=CARTESIAN_POINT ( 'NONE',  ( -33.72168855820452649, 11.47316190337362585, -176.7499999999999716 ) ) ;
#218279=VERTEX_POINT ( 'NONE', #167 ) ;
#218425=ORIENTED_EDGE ( 'NONE', *, *, #229768, .T. ) ;
#218803=CARTESIAN_POINT ( 'NONE',  ( -16.91256925476571382, 9.985731158139332209, -180.0323575109946717 ) ) ;
#218883=VECTOR ( 'NONE', #223013, 1000.000000000000000 ) ;
#219073=CARTESIAN_POINT ( 'NONE',  ( -16.94107738177414291, 10.01423928514777373, -188.4499999999999886 ) ) ;
#219278=EDGE_CURVE ( 'NONE', #222610, #231369, #235095, .T. ) ;
#219289=CARTESIAN_POINT ( 'NONE',  ( -16.89935556175728593, 9.950000000011264945, -187.8603236371162950 ) ) ;
#219549=CARTESIAN_POINT ( 'NONE',  ( -15.52965525596986929, 9.375538102059156387, -183.3698758809907474 ) ) ;
#219570=ORIENTED_EDGE ( 'NONE', *, *, #232251, .T. ) ;
#219577=ORIENTED_EDGE ( 'NONE', *, *, #229107, .F. ) ;
#219754=CARTESIAN_POINT ( 'NONE',  ( 14.45204356427542791, 9.450668889178684751, -182.5555464902073197 ) ) ;
#219840=FILL_AREA_STYLE_COLOUR ( '', #214629 ) ;
#219960=VECTOR ( 'NONE', #138223, 1000.000000000000000 ) ;
#220261=CARTESIAN_POINT ( 'NONE',  ( -17.11825945287481332, 9.950000000011138823, -188.2499999999999716 ) ) ;
#220307=CARTESIAN_POINT ( 'NONE',  ( 15.31784899511109188, 9.396630376328875656, -185.4070573928183308 ) ) ;
#220363=ORIENTED_EDGE ( 'NONE', *, *, #84751, .T. ) ;
#220485=CARTESIAN_POINT ( 'NONE',  ( -16.87333278164158656, 9.882609784590076885, -180.6331678061535797 ) ) ;
#220791=VERTEX_POINT ( 'NONE', #246291 ) ;
#220839=CARTESIAN_POINT ( 'NONE',  ( -15.39946565075089779, 9.389534562357860992, -183.1748093043898962 ) ) ;
#220874=VERTEX_POINT ( 'NONE', #46779 ) ;
#221170=PLANE ( 'NONE',  #171146 ) ;
#221277=CARTESIAN_POINT ( 'NONE',  ( -18.37013991200266361, 11.49974761622313579, -191.7930230105170892 ) ) ;
#221315=DIRECTION ( 'NONE',  ( 0.000000000000000000, 0.000000000000000000, -1.000000000000000000 ) ) ;
#221350=LINE ( 'NONE', #244771, #33637 ) ;
#221448=VECTOR ( 'NONE', #236951, 1000.000000000000000 ) ;
#221476=CARTESIAN_POINT ( 'NONE',  ( -18.40000000000000213, 11.75000000001113953, -188.3499999999999659 ) ) ;
#221608=CARTESIAN_POINT ( 'NONE',  ( -16.89146115310545682, 9.951443245667611848, -188.3548224189541997 ) ) ;
#221716=CARTESIAN_POINT ( 'NONE',  ( -16.77902162784673834, 9.946419257218995114, -180.1619912440693270 ) ) ;
#221900=FACE_OUTER_BOUND ( 'NONE', #59177, .T. ) ;
#222073=DIRECTION ( 'NONE',  ( -0.000000000000000000, -0.000000000000000000, -1.000000000000000000 ) ) ;
#222147=ORIENTED_EDGE ( 'NONE', *, *, #55800, .F. ) ;
#222296=EDGE_CURVE ( 'NONE', #232305, #235554, #139183, .T. ) ;
#222313=ADVANCED_FACE ( 'NONE', ( #117087 ), #257816, .F. ) ;
#222433=B_SPLINE_CURVE_WITH_KNOTS ( 'NONE', 3,
 ( #5061, #243705, #239868, #61218, #39112, #140752, #118649, #59908, #220307, #228958, #224129, #32062, #171578, #211972, #65066, #251067, #230233, #189830, #111578, #29506, #149439, #144586, #69904, #45503, #50294, #132427, #92002, #12493, #90713, #30779 ),
 .UNSPECIFIED., .F., .F.,
 ( 4, 2, 2, 2, 2, 2, 2, 2, 2, 2, 2, 2, 2, 2, 4 ),
 ( 0.000000000000000000, 0.0003422764154113552447, 0.0006845528308227104893, 0.001026829246234067794, 0.001369105661645424882, 0.002053658492468080510, 0.002738211323290736139, 0.003080487738702061135, 0.003422764154113386997, 0.003765040569524712426, 0.004107316984936037856, 0.004449593400347363718, 0.004791869815758688714, 0.005134146231170014577, 0.005476422646581339572 ),
 .UNSPECIFIED. ) ;
#222448=CARTESIAN_POINT ( 'NONE',  ( -16.87331047859649757, 9.950000000011138823, -188.3499999999999659 ) ) ;
#222557=CARTESIAN_POINT ( 'NONE',  ( -18.41431012584567739, 11.48747202921933308, -191.7732360131016662 ) ) ;
#222559=CARTESIAN_POINT ( 'NONE',  ( -16.87036670365548474, 9.989418819312801290, -188.4795601173020145 ) ) ;
#222610=VERTEX_POINT ( 'NONE', #132485 ) ;
#222729=CARTESIAN_POINT ( 'NONE',  ( -17.78241384941336989, 10.85557575280576792, -177.7490376724458088 ) ) ;
#222915=ORIENTED_EDGE ( 'NONE', *, *, #300, .F. ) ;
#222919=CARTESIAN_POINT ( 'NONE',  ( -16.77683809663752257, 23.65833333334447985, -184.2499999999999716 ) ) ;
#222973=DIRECTION ( 'NONE',  ( -1.000000000000000000, 1.652117596168391700E-15, 0.000000000000000000 ) ) ;
#222974=ORIENTED_EDGE ( 'NONE', *, *, #162726, .T. ) ;
#223013=DIRECTION ( 'NONE',  ( -1.652117596168391700E-15, -1.000000000000000000, 0.000000000000000000 ) ) ;
#223051=SURFACE_STYLE_FILL_AREA ( #63988 ) ;
#223262=ORIENTED_EDGE ( 'NONE', *, *, #4786, .F. ) ;
#223281=CARTESIAN_POINT ( 'NONE',  ( -16.88495309932523369, 9.954627058484017965, -180.1345486738118780 ) ) ;
#223940=CARTESIAN_POINT ( 'NONE',  ( -20.65000000000000568, 5.650000000011139001, -176.7499999999999716 ) ) ;
#224015=CARTESIAN_POINT ( 'NONE',  ( -18.44085059012131822, 11.51401249349495437, -176.7596946808784253 ) ) ;
#224124=DIRECTION ( 'NONE',  ( 0.7071067811865456854, -0.7071067811865493491, -0.000000000000000000 ) ) ;
#224129=CARTESIAN_POINT ( 'NONE',  ( 14.88075390448864610, 9.431689550535256927, -185.7792900322359912 ) ) ;
#224136=ORIENTED_EDGE ( 'NONE', *, *, #235329, .F. ) ;
#224374=VECTOR ( 'NONE', #80476, 1000.000000000000000 ) ;
#224424=CARTESIAN_POINT ( 'NONE',  ( -16.80891096016325292, 9.950000000011137047, -188.3676628072681183 ) ) ;
#224554=LINE ( 'NONE', #30231, #213650 ) ;
#224560=DIRECTION ( 'NONE',  ( 1.186688945009010077E-16, -1.000000000000000000, -0.000000000000000000 ) ) ;
#224829=VERTEX_POINT ( 'NONE', #187460 ) ;
#224862=DIRECTION ( 'NONE',  ( -0.000000000000000000, 1.000000000000000000, -0.000000000000000000 ) ) ;
#224884=CARTESIAN_POINT ( 'NONE',  ( 12.93225390519045703, 9.417651958852161442, -182.8587873924404050 ) ) ;
#224991=ORIENTED_EDGE ( 'NONE', *, *, #135873, .F. ) ;
#225097=LINE ( 'NONE', #10911, #240677 ) ;
#225127=CARTESIAN_POINT ( 'NONE',  ( 20.73486653747088226, 7.250000000011182166, -180.1499999999999773 ) ) ;
#225377=DIRECTION ( 'NONE',  ( 0.000000000000000000, -1.000000000000000000, 0.000000000000000000 ) ) ;
#225451=ADVANCED_FACE ( 'NONE', ( #22327 ), #180104, .F. ) ;
#225527=CARTESIAN_POINT ( 'NONE',  ( 20.99999999999999645, 9.750000000011137757, -188.3499999999999659 ) ) ;
#225576=FACE_OUTER_BOUND ( 'NONE', #80756, .T. ) ;
#225580=ORIENTED_EDGE ( 'NONE', *, *, #84751, .F. ) ;
#225705=EDGE_CURVE ( 'NONE', #13877, #111909, #67714, .T. ) ;
#226226=VECTOR ( 'NONE', #224124, 1000.000000000000000 ) ;
#226229=EDGE_CURVE ( 'NONE', #13877, #257956, #66080, .T. ) ;
#226273=VECTOR ( 'NONE', #108798, 1000.000000000000000 ) ;
#226334=ORIENTED_EDGE ( 'NONE', *, *, #34671, .T. ) ;
#226412=( BOUNDED_CURVE ( )  B_SPLINE_CURVE ( 3, ( #251967, #73367, #94168, #154207 ),
 .UNSPECIFIED., .F., .T. ) 
 B_SPLINE_CURVE_WITH_KNOTS ( ( 4, 4 ),
 ( 1.570796326794885012, 3.141592653589794448 ),
 .UNSPECIFIED. ) 
 CURVE ( )  GEOMETRIC_REPRESENTATION_ITEM ( )  RATIONAL_B_SPLINE_CURVE ( ( 1.000000000000000000, 0.8047378541243619399, 0.8047378541243619399, 1.000000000000000000 ) ) 
 REPRESENTATION_ITEM ( '' )  );
#226743=AXIS2_PLACEMENT_3D ( 'NONE', #97922, #236177, #121 ) ;
#226874=CARTESIAN_POINT ( 'NONE',  ( -16.79814274880124358, 9.949272542688458287, -180.1524330370479845 ) ) ;
#226876=ORIENTED_EDGE ( 'NONE', *, *, #205184, .F. ) ;
#226882=CARTESIAN_POINT ( 'NONE',  ( -16.82055514392353501, 9.950000000011076651, -180.1767980745427167 ) ) ;
#226998=CARTESIAN_POINT ( 'NONE',  ( -16.87401514999227814, 9.950000000011137047, -188.2800179925320663 ) ) ;
#227074=CARTESIAN_POINT ( 'NONE',  ( -18.39999999999999858, 11.47867410001042998, -176.7746932163406086 ) ) ;
#227119=ADVANCED_FACE ( 'NONE', ( #195113, #238051, #112988 ), #93406, .T. ) ;
#227146=B_SPLINE_CURVE_WITH_KNOTS ( 'NONE', 3,
 ( #82584, #256060, #78752, #219549, #220839, #138702, #39675, #120498, #240418, #119191, #99586, #17503, #181729, #80016, #140005, #102150, #60473, #40960, #61775, #42223, #121773, #201281, #22676, #3064, #162185, #241696 ),
 .UNSPECIFIED., .F., .F.,
 ( 4, 2, 2, 2, 2, 2, 2, 2, 2, 2, 2, 2, 4 ),
 ( 0.005476422646581349113, 0.006160811967703574803, 0.006845201288825800492, 0.007187395949386913771, 0.007529590609948027050, 0.007871785270509140328, 0.008213979931070251872, 0.008556174591631365151, 0.008898369252192478429, 0.009240563912753591708, 0.009582758573314704986, 0.01026714789443687256, 0.01095153721555903840 ),
 .UNSPECIFIED. ) ;
#227155=ORIENTED_EDGE ( 'NONE', *, *, #77830, .T. ) ;
#227405=ORIENTED_EDGE ( 'NONE', *, *, #155753, .F. ) ;
#227418=CARTESIAN_POINT ( 'NONE',  ( -16.97092634996667471, 10.00088896635978308, -188.3698572337024757 ) ) ;
#227622=CARTESIAN_POINT ( 'NONE',  ( -16.27683809663751191, 9.350000000011133849, -176.7499999999999432 ) ) ;
#227804=ORIENTED_EDGE ( 'NONE', *, *, #17207, .F. ) ;
#227872=CARTESIAN_POINT ( 'NONE',  ( -15.51798037960204546, 9.376659938544687378, -185.1281925482172710 ) ) ;
#228095=CARTESIAN_POINT ( 'NONE',  ( -17.04295772865469871, 10.02489942527109612, -180.1499999999999773 ) ) ;
#228134=CARTESIAN_POINT ( 'NONE',  ( -16.81931177881023132, 9.936996059515061930, -188.2732178786172028 ) ) ;
#228381=CARTESIAN_POINT ( 'NONE',  ( -18.40000000000000213, 11.48667500176882328, -176.7499999999999716 ) ) ;
#228502=ORIENTED_EDGE ( 'NONE', *, *, #14011, .T. ) ;
#228655=FACE_OUTER_BOUND ( 'NONE', #80495, .T. ) ;
#228721=ORIENTED_EDGE ( 'NONE', *, *, #105194, .F. ) ;
#228958=CARTESIAN_POINT ( 'NONE',  ( 15.07585980824112148, 9.417632963117448242, -185.6489484657322180 ) ) ;
#229010=AXIS2_PLACEMENT_3D ( 'NONE', #115419, #236649, #13763 ) ;
#229107=EDGE_CURVE ( 'NONE', #71159, #57422, #86397, .T. ) ;
#229329=CIRCLE ( 'NONE', #154353, 0.09999999999999939493 ) ;
#229501=CARTESIAN_POINT ( 'NONE',  ( -20.65000000000000568, 7.250000000011138646, -180.1499999999999773 ) ) ;
#229514=ORIENTED_EDGE ( 'NONE', *, *, #155463, .T. ) ;
#229526=CARTESIAN_POINT ( 'NONE',  ( 20.09999999999999787, 9.750000000011137757, -180.1499999999999773 ) ) ;
#229573=ORIENTED_EDGE ( 'NONE', *, *, #191849, .T. ) ;
#229707=LINE ( 'NONE', #51026, #155023 ) ;
#229768=EDGE_CURVE ( 'NONE', #165955, #30570, #246487, .T. ) ;
#229860=FACE_OUTER_BOUND ( 'NONE', #149375, .T. ) ;
#230173=CARTESIAN_POINT ( 'NONE',  ( 15.74999999999999645, 9.850000000011137402, -184.2499999999999716 ) ) ;
#230197=CARTESIAN_POINT ( 'NONE',  ( -18.34374000495060386, 11.47316190337362585, -176.7499999999999716 ) ) ;
#230233=CARTESIAN_POINT ( 'NONE',  ( 13.43663047529819821, 9.446645344706400493, -185.9108064561001754 ) ) ;
#230311=CYLINDRICAL_SURFACE ( 'NONE', #136064, 0.09999999999999939493 ) ;
#230345=B_SPLINE_CURVE_WITH_KNOTS ( 'NONE', 3,
 ( #70613, #210107, #227074, #228381 ),
 .UNSPECIFIED., .F., .F.,
 ( 4, 4 ),
 ( 0.000000000000000000, 7.713889350930799751E-05 ),
 .UNSPECIFIED. ) ;
#230440=CARTESIAN_POINT ( 'NONE',  ( -15.73854595235692599, 9.351413679112548394, -184.4803435675489709 ) ) ;
#230529=DIRECTION ( 'NONE',  ( -1.073024830501117725E-15, -0.000000000000000000, -1.000000000000000000 ) ) ;
#230620=ORIENTED_EDGE ( 'NONE', *, *, #257479, .F. ) ;
#230637=ORIENTED_EDGE ( 'NONE', *, *, #243595, .F. ) ;
#230710=VECTOR ( 'NONE', #79593, 1000.000000000000000 ) ;
#230812=AXIS2_PLACEMENT_3D ( 'NONE', #32138, #94643, #192472 ) ;
#230846=CARTESIAN_POINT ( 'NONE',  ( -16.86133551771148831, 9.950000000011137047, -188.3013434345466806 ) ) ;
#231119=EDGE_LOOP ( 'NONE', ( #116744, #87813, #18410, #163284 ) ) ;
#231369=VERTEX_POINT ( 'NONE', #79360 ) ;
#231454=EDGE_LOOP ( 'NONE', ( #4635, #120954, #78333 ) ) ;
#231701=DIRECTION ( 'NONE',  ( -1.073024830501117725E-15, 0.000000000000000000, 1.000000000000000000 ) ) ;
#232044=CARTESIAN_POINT ( 'NONE',  ( -16.83558968593869665, 9.950000000011137047, -180.1623051876166812 ) ) ;
#232138=PRODUCT_DEFINITION_FORMATION_WITH_SPECIFIED_SOURCE ( 'ANY', '', #168068, .NOT_KNOWN. ) ;
#232238=VERTEX_POINT ( 'NONE', #86117 ) ;
#232251=EDGE_CURVE ( 'NONE', #43046, #250008, #191010, .T. ) ;
#232268=CARTESIAN_POINT ( 'NONE',  ( -18.40000000000000213, 11.47316190337310537, -191.7001707515342446 ) ) ;
#232305=VERTEX_POINT ( 'NONE', #229526 ) ;
#232409=CARTESIAN_POINT ( 'NONE',  ( -16.87036670365549895, 10.08494996326643189, -180.0499999999999545 ) ) ;
#232668=CARTESIAN_POINT ( 'NONE',  ( -16.94132844910802405, 9.992436755191501874, -188.3962017559823039 ) ) ;
#232835=FACE_OUTER_BOUND ( 'NONE', #206111, .T. ) ;
#232892=ORIENTED_EDGE ( 'NONE', *, *, #29386, .T. ) ;
#232954=CARTESIAN_POINT ( 'NONE',  ( -33.72168855820452649, 23.65833333334447985, -184.2499999999999716 ) ) ;
#233054=ORIENTED_EDGE ( 'NONE', *, *, #229107, .T. ) ;
#233388=ORIENTED_EDGE ( 'NONE', *, *, #33345, .F. ) ;
#233623=EDGE_CURVE ( 'NONE', #156996, #33770, #229329, .T. ) ;
#233688=CARTESIAN_POINT ( 'NONE',  ( -16.89268316805466341, 9.951721813253341153, -180.1442475214544174 ) ) ;
#233703=CARTESIAN_POINT ( 'NONE',  ( -17.11825945287481332, 10.05000000001113847, -188.3499999999999659 ) ) ;
#233725=EDGE_CURVE ( 'NONE', #131422, #86347, #125276, .T. ) ;
#233962=ORIENTED_EDGE ( 'NONE', *, *, #77672, .F. ) ;
#234137=DIRECTION ( 'NONE',  ( 0.000000000000000000, -1.000000000000000000, 0.000000000000000000 ) ) ;
#234408=CARTESIAN_POINT ( 'NONE',  ( -23.25000000000000355, 10.05000000001113847, -180.2499999999999716 ) ) ;
#234970=CARTESIAN_POINT ( 'NONE',  ( -16.87487986503753845, 9.950007555096753720, -180.1499747396866837 ) ) ;
#235095=B_SPLINE_CURVE_WITH_KNOTS ( 'NONE', 3,
 ( #83440, #87309, #144714, #41806, #84714, #161752, #164309 ),
 .UNSPECIFIED., .F., .F.,
 ( 4, 3, 4 ),
 ( 0.000000000000000000, 4.520325912680675723E-05, 5.794988040901448781E-05 ),
 .UNSPECIFIED. ) ;
#235221=ORIENTED_EDGE ( 'NONE', *, *, #143935, .T. ) ;
#235329=EDGE_CURVE ( 'NONE', #134738, #218279, #101056, .T. ) ;
#235554=VERTEX_POINT ( 'NONE', #211397 ) ;
#235612=CARTESIAN_POINT ( 'NONE',  ( 12.25000000000000000, 9.850000000011137402, -184.2499999999999716 ) ) ;
#235634=ADVANCED_FACE ( 'NONE', ( #177436 ), #38, .F. ) ;
#236058=CARTESIAN_POINT ( 'NONE',  ( -16.87331047859649757, 9.950000000011138823, -188.3499999999999659 ) ) ;
#236177=DIRECTION ( 'NONE',  ( 0.000000000000000000, 0.000000000000000000, 1.000000000000000000 ) ) ;
#236274=LINE ( 'NONE', #139726, #59379 ) ;
#236287=CARTESIAN_POINT ( 'NONE',  ( -16.96982749440706328, 9.950000000011137047, -187.8752215911892165 ) ) ;
#236649=DIRECTION ( 'NONE',  ( -0.000000000000000000, -0.000000000000000000, -1.000000000000000000 ) ) ;
#236674=DIRECTION ( 'NONE',  ( -0.000000000000000000, -0.000000000000000000, -1.000000000000000000 ) ) ;
#236694=ORIENTED_EDGE ( 'NONE', *, *, #219278, .F. ) ;
#236792=ORIENTED_EDGE ( 'NONE', *, *, #75961, .T. ) ;
#236939=EDGE_CURVE ( 'NONE', #131422, #68352, #96987, .T. ) ;
#236951=DIRECTION ( 'NONE',  ( -0.000000000000000000, -0.000000000000000000, -1.000000000000000000 ) ) ;
#236961=EDGE_CURVE ( 'NONE', #172479, #171571, #255328, .T. ) ;
#237031=CARTESIAN_POINT ( 'NONE',  ( 21.72449340488910252, 10.28395627750227526, -176.7499999999999716 ) ) ;
#237176=DIRECTION ( 'NONE',  ( 1.000000000000000000, 0.000000000000000000, 0.000000000000000000 ) ) ;
#237291=EDGE_CURVE ( 'NONE', #56614, #136660, #89566, .T. ) ;
#237353=LINE ( 'NONE', #200792, #74442 ) ;
#237469=CARTESIAN_POINT ( 'NONE',  ( -16.93339986808596365, 10.00510392857707487, -180.0659936718128336 ) ) ;
#237508=EDGE_CURVE ( 'NONE', #71159, #8352, #11330, .T. ) ;
#237649=ORIENTED_EDGE ( 'NONE', *, *, #239552, .T. ) ;
#238045=ORIENTED_EDGE ( 'NONE', *, *, #300, .T. ) ;
#238051=FACE_BOUND ( 'NONE', #211498, .T. ) ;
#238110=EDGE_LOOP ( 'NONE', ( #84192, #104607, #64162, #255194 ) ) ;
#238152=CARTESIAN_POINT ( 'NONE',  ( -16.94445028196808778, 9.992063609708889516, -180.1073301784184366 ) ) ;
#238375=CARTESIAN_POINT ( 'NONE',  ( -16.86445178670579992, 9.962211629127164514, -180.1092225618826319 ) ) ;
#238553=ORIENTED_EDGE ( 'NONE', *, *, #63235, .T. ) ;
#238634=CARTESIAN_POINT ( 'NONE',  ( -16.87665923198281348, 9.950000000011138823, -188.3499999999999659 ) ) ;
#238979=CARTESIAN_POINT ( 'NONE',  ( -17.29158576265544056, 10.36474766602906783, -178.9172417552077832 ) ) ;
#238992=CARTESIAN_POINT ( 'NONE',  ( -17.05016517655587904, 9.950000000007385381, -188.3273020040059293 ) ) ;
#239137=DIRECTION ( 'NONE',  ( -1.000000000000000000, 0.000000000000000000, 0.000000000000000000 ) ) ;
#239336=CARTESIAN_POINT ( 'NONE',  ( 15.52844286134408236, 9.375669526436931633, -183.3677900093859989 ) ) ;
#239382=VERTEX_POINT ( 'NONE', #158762 ) ;
#239552=EDGE_CURVE ( 'NONE', #185125, #56614, #225097, .T. ) ;
#239673=CARTESIAN_POINT ( 'NONE',  ( -16.93935632781549572, 9.984730499736244269, -188.3896607487102699 ) ) ;
#239797=PLANE ( 'NONE',  #112358 ) ;
#239868=CARTESIAN_POINT ( 'NONE',  ( 15.73863059295127798, 9.351403174152808973, -184.4795304368384734 ) ) ;
#239928=CARTESIAN_POINT ( 'NONE',  ( -16.89081410710458542, 9.951318529858268036, -188.3544059198363527 ) ) ;
#239939=LINE ( 'NONE', #116142, #254572 ) ;
#240164=ADVANCED_FACE ( 'NONE', ( #6420 ), #41726, .F. ) ;
#240352=DIRECTION ( 'NONE',  ( 0.000000000000000000, 0.000000000000000000, -1.000000000000000000 ) ) ;
#240418=CARTESIAN_POINT ( 'NONE',  ( -14.77738660682463667, 9.436552840015577814, -182.6779554727602886 ) ) ;
#240527=AXIS2_PLACEMENT_3D ( 'NONE', #227622, #107681, #183383 ) ;
#240677=VECTOR ( 'NONE', #52579, 1000.000000000000000 ) ;
#240744=DIRECTION ( 'NONE',  ( 1.000000000000000000, 0.000000000000000000, -0.000000000000000000 ) ) ;
#240812=LINE ( 'NONE', #82976, #48209 ) ;
#241035=DIRECTION ( 'NONE',  ( 0.000000000000000000, 1.000000000000000000, -0.000000000000000000 ) ) ;
#241215=DIRECTION ( 'NONE',  ( -0.5932847527679299127, 0.8049926720990051576, 6.366092712777055223E-16 ) ) ;
#241264=EDGE_LOOP ( 'NONE', ( #56892, #97423, #89921, #1511 ) ) ;
#241295=LINE ( 'NONE', #61352, #121048 ) ;
#241303=CARTESIAN_POINT ( 'NONE',  ( 23.24999999999999645, 11.75000000001113953, -188.3499999999999659 ) ) ;
#241344=ORIENTED_EDGE ( 'NONE', *, *, #34671, .F. ) ;
#241576=EDGE_LOOP ( 'NONE', ( #83874, #228502 ) ) ;
#241696=CARTESIAN_POINT ( 'NONE',  ( -12.25000000000000178, 9.350000000011139178, -184.2499999999999716 ) ) ;
#241870=VERTEX_POINT ( 'NONE', #190834 ) ;
#241975=SURFACE_STYLE_USAGE ( .BOTH. , #103719 ) ;
#242059=VECTOR ( 'NONE', #6088, 1000.000000000000000 ) ;
#242134=CARTESIAN_POINT ( 'NONE',  ( -16.94107738177413580, 10.01423928514777195, -188.4499999999999602 ) ) ;
#242348=CARTESIAN_POINT ( 'NONE',  ( 23.24999999999999645, 8.822561741677553471, -180.1499999999999773 ) ) ;
#242580=CARTESIAN_POINT ( 'NONE',  ( -21.64999999999999858, 9.350000000011133849, -180.1499999999999773 ) ) ;
#242702=CARTESIAN_POINT ( 'NONE',  ( -16.80621392010912629, 9.942202577518866491, -188.3104080345828208 ) ) ;
#242802=ORIENTED_EDGE ( 'NONE', *, *, #109384, .T. ) ;
#242872=CARTESIAN_POINT ( 'NONE',  ( 17.23472005113828232, 10.30788195451192379, -178.9534231399312887 ) ) ;
#243110=VERTEX_POINT ( 'NONE', #129877 ) ;
#243194=DIRECTION ( 'NONE',  ( -1.000000000000000000, 0.000000000000000000, 0.000000000000000000 ) ) ;
#243423=LINE ( 'NONE', #225127, #242059 ) ;
#243584=ORIENTED_EDGE ( 'NONE', *, *, #180388, .F. ) ;
#243595=EDGE_CURVE ( 'NONE', #10681, #51363, #239939, .T. ) ;
#243622=ORIENTED_EDGE ( 'NONE', *, *, #8766, .T. ) ;
#243705=CARTESIAN_POINT ( 'NONE',  ( 15.74999999999999645, 9.350000000011139178, -184.3657431672739051 ) ) ;
#243793=CARTESIAN_POINT ( 'NONE',  ( -17.11825945287483108, 9.950000000011112178, -180.1499999999999488 ) ) ;
#243819=CARTESIAN_POINT ( 'NONE',  ( 18.39999999999999503, 11.75000000001113953, -180.1499999999999773 ) ) ;
#243948=DIRECTION ( 'NONE',  ( 1.000000000000000000, 0.000000000000000000, 0.000000000000000000 ) ) ;
#244261=VERTEX_POINT ( 'NONE', #11277 ) ;
#244377=LINE ( 'NONE', #217420, #197705 ) ;
#244457=CARTESIAN_POINT ( 'NONE',  ( 14.11444803880197441, 9.457431528860068326, -182.4999169378996555 ) ) ;
#244771=CARTESIAN_POINT ( 'NONE',  ( -23.25000000000000355, 5.650000000011139001, -188.3499999999999659 ) ) ;
#244868=CARTESIAN_POINT ( 'NONE',  ( -16.81744102076748959, 9.950000000011138823, -188.3499999999999659 ) ) ;
#245010=CARTESIAN_POINT ( 'NONE',  ( 13.99999999999999822, 9.850000000011137402, -184.2499999999999716 ) ) ;
#245052=ORIENTED_EDGE ( 'NONE', *, *, #168921, .F. ) ;
#245077=CARTESIAN_POINT ( 'NONE',  ( -16.97092634996677774, 10.00088896635983460, -180.1301427662975243 ) ) ;
#245103=EDGE_LOOP ( 'NONE', ( #160889, #151596, #201597, #254064 ) ) ;
#245115=VECTOR ( 'NONE', #166390, 1000.000000000000000 ) ;
#245425=PLANE ( 'NONE',  #151122 ) ;
#245457=CARTESIAN_POINT ( 'NONE',  ( 18.39999999999998082, 11.47316190337362585, -176.7499999999999716 ) ) ;
#245607=LINE ( 'NONE', #66960, #181453 ) ;
#245673=LINE ( 'NONE', #166171, #20591 ) ;
#245726=EDGE_LOOP ( 'NONE', ( #192332, #224136, #13602, #204244, #236694 ) ) ;
#246048=EDGE_LOOP ( 'NONE', ( #207969, #50434, #96265, #75724 ) ) ;
#246142=FACE_OUTER_BOUND ( 'NONE', #159010, .T. ) ;
#246250=CARTESIAN_POINT ( 'NONE',  ( -21.64999999999999858, 10.05000000001113847, -188.2499999999999716 ) ) ;
#246291=CARTESIAN_POINT ( 'NONE',  ( -23.25000000000000355, 11.75000000001113953, -180.1499999999999773 ) ) ;
#246467=CARTESIAN_POINT ( 'NONE',  ( -18.36973785203556275, 11.47550320049537476, -191.7499999999999716 ) ) ;
#246487=LINE ( 'NONE', #9167, #128104 ) ;
#246504=DIRECTION ( 'NONE',  ( 1.000000000000000000, 0.000000000000000000, 0.000000000000000000 ) ) ;
#246551=CARTESIAN_POINT ( 'NONE',  ( -16.80070461187835562, 9.950000000011328893, -188.3530361708423868 ) ) ;
#246564=DIRECTION ( 'NONE',  ( -1.000000000000000000, 0.000000000000000000, -0.000000000000000000 ) ) ;
#246617=CARTESIAN_POINT ( 'NONE',  ( -23.25000000000000355, 11.75000000001113953, -176.7499999999999716 ) ) ;
#246693=CARTESIAN_POINT ( 'NONE',  ( -14.00000000000000178, 9.850000000011133849, -184.2499999999999716 ) ) ;
#246725=CARTESIAN_POINT ( 'NONE',  ( 20.73486653747088937, 7.750000000011182166, -176.7499999999999716 ) ) ;
#247183=CARTESIAN_POINT ( 'NONE',  ( 18.39999999999999503, 11.75000000001113953, -180.1499999999999773 ) ) ;
#247233=VERTEX_POINT ( 'NONE', #71814 ) ;
#247309=CARTESIAN_POINT ( 'NONE',  ( 13.99999999999999822, 9.850000000011137402, -184.2499999999999716 ) ) ;
#247407=DIRECTION ( 'NONE',  ( -1.000000000000000000, 0.000000000000000000, -1.020425574104004196E-15 ) ) ;
#247686=CARTESIAN_POINT ( 'NONE',  ( -16.85312964099708566, 9.913604682078865693, -188.1028157064303912 ) ) ;
#248137=ORIENTED_EDGE ( 'NONE', *, *, #77672, .T. ) ;
#248393=VERTEX_POINT ( 'NONE', #10908 ) ;
#248529=ORIENTED_EDGE ( 'NONE', *, *, #82133, .T. ) ;
#248646=CARTESIAN_POINT ( 'NONE',  ( -16.92563707711778065, 9.968990694407935393, -188.3807582995239329 ) ) ;
#248831=EDGE_CURVE ( 'NONE', #1714, #167528, #182281, .T. ) ;
#248901=AXIS2_PLACEMENT_3D ( 'NONE', #254077, #195423, #14221 ) ;
#248943=CARTESIAN_POINT ( 'NONE',  ( -17.01764560440330953, 9.950000000011138823, -180.2499999992110702 ) ) ;
#248993=EDGE_CURVE ( 'NONE', #104626, #171694, #243423, .T. ) ;
#249116=PLANE ( 'NONE',  #118777 ) ;
#249138=VECTOR ( 'NONE', #222073, 1000.000000000000000 ) ;
#249277=FACE_OUTER_BOUND ( 'NONE', #210487, .T. ) ;
#249360=DIRECTION ( 'NONE',  ( 1.000000000000000000, 1.186688945009009831E-16, 0.000000000000000000 ) ) ;
#249422=CARTESIAN_POINT ( 'NONE',  ( -17.11825945287482753, 9.950000000011138823, -180.2499999999999716 ) ) ;
#249616=CARTESIAN_POINT ( 'NONE',  ( 12.25000000000000000, 9.850000000011137402, -184.2499999999999716 ) ) ;
#249653=ORIENTED_EDGE ( 'NONE', *, *, #225705, .F. ) ;
#250003=CARTESIAN_POINT ( 'NONE',  ( -12.33960340485503870, 9.360749169926261715, -184.8145701406072874 ) ) ;
#250008=VERTEX_POINT ( 'NONE', #121576 ) ;
#250301=CARTESIAN_POINT ( 'NONE',  ( -16.80070461187954578, 9.950000000010851053, -180.1469638291620186 ) ) ;
#250521=ORIENTED_EDGE ( 'NONE', *, *, #131792, .F. ) ;
#250660=CARTESIAN_POINT ( 'NONE',  ( -16.87683809663752399, 9.850000000011144508, -180.9023640181962662 ) ) ;
#250694=CARTESIAN_POINT ( 'NONE',  ( -21.65000000000000213, 7.250000000011138646, -176.7499999999999716 ) ) ;
#250812=ADVANCED_FACE ( 'NONE', ( #21822 ), #206219, .T. ) ;
#250835=AXIS2_PLACEMENT_3D ( 'NONE', #102515, #3439, #79118 ) ;
#250855=AXIS2_PLACEMENT_3D ( 'NONE', #131670, #33910, #174704 ) ;
#250931=LINE ( 'NONE', #211837, #90692 ) ;
#251067=CARTESIAN_POINT ( 'NONE',  ( 13.54577453029516043, 9.450602096099679272, -185.9438959630965655 ) ) ;
#251293=ORIENTED_EDGE ( 'NONE', *, *, #83020, .T. ) ;
#251519=CIRCLE ( 'NONE', #255568, 1.749999999999999778 ) ;
#251718=FACE_OUTER_BOUND ( 'NONE', #166923, .T. ) ;
#251967=CARTESIAN_POINT ( 'NONE',  ( -18.40000000000000213, 11.33174054713631662, -180.1499999999999773 ) ) ;
#252021=ADVANCED_FACE ( 'NONE', ( #180935 ), #2271, .F. ) ;
#252041=CARTESIAN_POINT ( 'NONE',  ( 18.39999999999997371, 11.47316190337362940, -191.7499999999999716 ) ) ;
#252117=CARTESIAN_POINT ( 'NONE',  ( -16.87242674293849731, 9.950000000011138823, -188.3510902463723369 ) ) ;
#252176=ADVANCED_FACE ( 'NONE', ( #167815 ), #109082, .T. ) ;
#252455=CIRCLE ( 'NONE', #210780, 1.749999999999998002 ) ;
#252488=ORIENTED_EDGE ( 'NONE', *, *, #105567, .F. ) ;
#252618=PLANE ( 'NONE',  #200064 ) ;
#252619=VECTOR ( 'NONE', #26474, 999.9999999999998863 ) ;
#252713=AXIS2_PLACEMENT_3D ( 'NONE', #185621, #27865, #166092 ) ;
#252724=EDGE_CURVE ( 'NONE', #171479, #156996, #71809, .T. ) ;
#253699=UNCERTAINTY_MEASURE_WITH_UNIT (LENGTH_MEASURE( 1.000000000000000082E-05 ), #80301, 'distance_accuracy_value', 'NONE');
#253982=ORIENTED_EDGE ( 'NONE', *, *, #167886, .T. ) ;
#254002=AXIS2_PLACEMENT_3D ( 'NONE', #53804, #10832, #167362 ) ;
#254010=PRODUCT_DEFINITION_CONTEXT ( 'detailed design', #77473, 'design' ) ;
#254064=ORIENTED_EDGE ( 'NONE', *, *, #125197, .F. ) ;
#254077=CARTESIAN_POINT ( 'NONE',  ( 23.04999999999999716, 8.822561741677553471, -176.7499999999999716 ) ) ;
#254251=CARTESIAN_POINT ( 'NONE',  ( -16.78805706634180339, 9.948252493082335945, -188.3441532080318268 ) ) ;
#254434=CARTESIAN_POINT ( 'NONE',  ( -16.94062896051973865, 9.992719105111833144, -180.1025165421187637 ) ) ;
#254442=LINE ( 'NONE', #75836, #25816 ) ;
#254507=CARTESIAN_POINT ( 'NONE',  ( -16.87683809663752399, 9.850000000011144508, -187.5976359818036769 ) ) ;
#254572=VECTOR ( 'NONE', #196939, 999.9999999999998863 ) ;
#254621=DIRECTION ( 'NONE',  ( 1.186688945009010077E-16, -1.000000000000000000, -0.000000000000000000 ) ) ;
#254627=ORIENTED_EDGE ( 'NONE', *, *, #40615, .T. ) ;
#254729=CARTESIAN_POINT ( 'NONE',  ( -16.94107738177414291, 10.01423928514777373, -188.4499999999999886 ) ) ;
#254777=EDGE_CURVE ( 'NONE', #100115, #134738, #115424, .T. ) ;
#254927=CARTESIAN_POINT ( 'NONE',  ( 18.54999999999999716, 8.750000000011182166, -188.3499999999999659 ) ) ;
#255194=ORIENTED_EDGE ( 'NONE', *, *, #156226, .T. ) ;
#255271=CARTESIAN_POINT ( 'NONE',  ( -16.27683809663751191, 9.350000000011132073, -180.0499999999999545 ) ) ;
#255276=VERTEX_POINT ( 'NONE', #172151 ) ;
#255319=ORIENTED_EDGE ( 'NONE', *, *, #207088, .T. ) ;
#255328=LINE ( 'NONE', #151166, #6157 ) ;
#255568=AXIS2_PLACEMENT_3D ( 'NONE', #200801, #102960, #59978 ) ;
#255643=PLANE ( 'NONE',  #14056 ) ;
#255660=ORIENTED_EDGE ( 'NONE', *, *, #71531, .T. ) ;
#255697=CARTESIAN_POINT ( 'NONE',  ( -16.94107738177415712, 10.01423928514777728, -180.0499999999999545 ) ) ;
#255766=CARTESIAN_POINT ( 'NONE',  ( -16.97683809663752186, 9.950000000011138823, -176.7499999999999716 ) ) ;
#255808=CARTESIAN_POINT ( 'NONE',  ( -16.97683809663752186, 9.950000000011137047, -187.5976359818036485 ) ) ;
#255812=DIRECTION ( 'NONE',  ( -1.000000000000000000, 0.000000000000000000, 0.000000000000000000 ) ) ;
#255842=CARTESIAN_POINT ( 'NONE',  ( -17.22361732159831504, 10.34515565861358866, -189.6292154741328204 ) ) ;
#255921=CARTESIAN_POINT ( 'NONE',  ( -17.11825945287481687, 9.950000000011167245, -188.3499999999999375 ) ) ;
#255966=CIRCLE ( 'NONE', #147698, 1.749999999999999778 ) ;
#256060=CARTESIAN_POINT ( 'NONE',  ( -15.75000000000000711, 9.350000000011142731, -184.0215193718251214 ) ) ;
#256129=EDGE_CURVE ( 'NONE', #158360, #46992, #236274, .T. ) ;
#256602=CARTESIAN_POINT ( 'NONE',  ( -16.87036670365549895, 9.989418819312803066, -180.0204398826979286 ) ) ;
#256737=CARTESIAN_POINT ( 'NONE',  ( -16.89268316805466341, 9.951721813253341153, -180.1442475214544174 ) ) ;
#256878=CARTESIAN_POINT ( 'NONE',  ( -16.86445178670582479, 9.962211629127164514, -188.3907774381173112 ) ) ;
#257087=FACE_OUTER_BOUND ( 'NONE', #164221, .T. ) ;
#257254=ORIENTED_EDGE ( 'NONE', *, *, #192639, .T. ) ;
#257478=ADVANCED_FACE ( 'NONE', ( #155400 ), #195800, .T. ) ;
#257479=EDGE_CURVE ( 'NONE', #257956, #134738, #206901, .T. ) ;
#257515=CYLINDRICAL_SURFACE ( 'NONE', #126669, 0.09999999999998898659 ) ;
#257677=ADVANCED_FACE ( 'NONE', ( #225576 ), #197832, .F. ) ;
#257713=CARTESIAN_POINT ( 'NONE',  ( -18.40000000000000213, 11.33174054713633261, -188.3499999999999659 ) ) ;
#257816=PLANE ( 'NONE',  #53509 ) ;
#257956=VERTEX_POINT ( 'NONE', #184878 ) ;
#258075=CARTESIAN_POINT ( 'NONE',  ( -16.77828822459933633, 9.946229375067616729, -188.3373717490810293 ) ) ;
ENDSEC;
END-ISO-10303-21;
